ISO-10303-21;
HEADER;
FILE_DESCRIPTION (('STEP AP203'),
    '1' );
FILE_NAME ('Tape Measure Hook.step',
    '2026-10-08T23:54:15',
    ( '' ),
    ( '' ),
    'SwSTEP 2.0',
    'SolidWorks 2024',
    '' );
FILE_SCHEMA (( 'AUTOMOTIVE_DESIGN' ));
ENDSEC;

DATA;
#1=EDGE_LOOP ( 'NONE', ( #69285, #69519, #6373, #20333 ) ) ;
#10=AXIS2_PLACEMENT_3D ( 'NONE', #33191, #48429, #34700 ) ;
#63=DIRECTION ( 'NONE',  ( -0.9762960071199348056, -0.2164396139380966033, -0.000000000000000000 ) ) ;
#186=LINE ( 'NONE', #37749, #11453 ) ;
#201=VECTOR ( 'NONE', #49390, 1000.000000000000000 ) ;
#287=CARTESIAN_POINT ( 'NONE',  ( -3.212051231530180573, 17.72614232434105119, -9.000000000000000000 ) ) ;
#292=ADVANCED_FACE ( 'NONE', ( #39393 ), #87066, .F. ) ;
#567=DIRECTION ( 'NONE',  ( -1.000000000000000000, 0.000000000000000000, -3.469446951953617147E-16 ) ) ;
#619=ADVANCED_FACE ( 'NONE', ( #75826 ), #60135, .F. ) ;
#907=DIRECTION ( 'NONE',  ( -1.000000000000000000, 0.000000000000000000, -4.956352788505167212E-16 ) ) ;
#1138=ORIENTED_EDGE ( 'NONE', *, *, #17846, .F. ) ;
#1211=CARTESIAN_POINT ( 'NONE',  ( 3.138110291115776995, 11.54688212118755075, -3.549999999999999822 ) ) ;
#1333=DIRECTION ( 'NONE',  ( 0.1478094111296165969, -0.9890158633619159367, 0.000000000000000000 ) ) ;
#1394=EDGE_LOOP ( 'NONE', ( #50435, #9530, #4530, #16937 ) ) ;
#1533=CARTESIAN_POINT ( 'NONE',  ( 0.000000000000000000, 0.000000000000000000, 0.000000000000000000 ) ) ;
#1549=VERTEX_POINT ( 'NONE', #83706 ) ;
#1619=PLANE ( 'NONE',  #50199 ) ;
#1657=VERTEX_POINT ( 'NONE', #88224 ) ;
#1781=VERTEX_POINT ( 'NONE', #13943 ) ;
#1930=CARTESIAN_POINT ( 'NONE',  ( 0.4923289614720766649, -7.060444313164428998, -9.000000000000000000 ) ) ;
#1984=DIRECTION ( 'NONE',  ( 0.000000000000000000, 1.000000000000000000, -6.307606751056558338E-17 ) ) ;
#2096=ORIENTED_EDGE ( 'NONE', *, *, #31922, .F. ) ;
#2154=ORIENTED_EDGE ( 'NONE', *, *, #72761, .T. ) ;
#2237=CARTESIAN_POINT ( 'NONE',  ( 1.255616527394258553, 17.95615290467683778, 9.000000000000000000 ) ) ;
#2289=DIRECTION ( 'NONE',  ( 0.000000000000000000, -1.000000000000000000, 4.688851412615178005E-17 ) ) ;
#2347=CYLINDRICAL_SURFACE ( 'NONE', #61988, 1.999999999999963141 ) ;
#2422=CARTESIAN_POINT ( 'NONE',  ( 1.876957540558651605, -5.558144974487054135, 0.000000000000000000 ) ) ;
#2481=CARTESIAN_POINT ( 'NONE',  ( 3.138110291115776995, 11.54688212118755075, -3.549999999999999822 ) ) ;
#2642=ORIENTED_EDGE ( 'NONE', *, *, #30266, .T. ) ;
#2779=CARTESIAN_POINT ( 'NONE',  ( -0.7395115731254252589, 18.09566585216508727, -9.000000000000000000 ) ) ;
#2990=VERTEX_POINT ( 'NONE', #91209 ) ;
#3060=DIRECTION ( 'NONE',  ( 0.9975640502598241977, -0.06975647374412546897, -0.000000000000000000 ) ) ;
#3098=CARTESIAN_POINT ( 'NONE',  ( -3.212051231530180573, 17.72614232434105119, 9.000000000000000000 ) ) ;
#3104=EDGE_CURVE ( 'NONE', #19708, #1781, #7466, .T. ) ;
#3208=EDGE_LOOP ( 'NONE', ( #32083, #72723, #89118, #65795 ) ) ;
#3310=ORIENTED_EDGE ( 'NONE', *, *, #42800, .F. ) ;
#3374=AXIS2_PLACEMENT_3D ( 'NONE', #50621, #18660, #49635 ) ;
#3405=ORIENTED_EDGE ( 'NONE', *, *, #74947, .F. ) ;
#3442=ORIENTED_EDGE ( 'NONE', *, *, #25021, .T. ) ;
#3445=DIRECTION ( 'NONE',  ( 0.8788171126619707119, -0.4771587602595986910, 6.123031769111886291E-17 ) ) ;
#3501=DIRECTION ( 'NONE',  ( -1.084136044942898696E-16, -0.000000000000000000, 1.000000000000000000 ) ) ;
#3516=ORIENTED_EDGE ( 'NONE', *, *, #82014, .F. ) ;
#3867=CIRCLE ( 'NONE', #7102, 10.11363636363636331 ) ;
#3915=AXIS2_PLACEMENT_3D ( 'NONE', #55552, #32192, #71772 ) ;
#3992=CARTESIAN_POINT ( 'NONE',  ( -4.700032041049139409, -6.144890974841530351, -9.000000000000000000 ) ) ;
#4089=ADVANCED_FACE ( 'NONE', ( #71900, #39935 ), #47562, .T. ) ;
#4163=EDGE_LOOP ( 'NONE', ( #2096, #85260, #54188, #12523 ) ) ;
#4179=AXIS2_PLACEMENT_3D ( 'NONE', #81109, #3501, #49187 ) ;
#4530=ORIENTED_EDGE ( 'NONE', *, *, #10138, .T. ) ;
#4553=ORIENTED_EDGE ( 'NONE', *, *, #55894, .T. ) ;
#4584=CARTESIAN_POINT ( 'NONE',  ( 0.7395552074414002419, -5.331939213628640317, 9.000000000000000000 ) ) ;
#4587=DIRECTION ( 'NONE',  ( -0.9890158633619158257, -0.1478094111296165691, -0.000000000000000000 ) ) ;
#4631=ORIENTED_EDGE ( 'NONE', *, *, #29196, .T. ) ;
#4739=CARTESIAN_POINT ( 'NONE',  ( -2.169994883066378222, 10.75358048763950869, 3.549999999999999822 ) ) ;
#4813=DIRECTION ( 'NONE',  ( 4.335561085774420994E-16, 0.000000000000000000, -1.000000000000000000 ) ) ;
#4837=DIRECTION ( 'NONE',  ( -2.205762779227727030E-17, 9.949552925324065630E-17, 1.000000000000000000 ) ) ;
#4862=ORIENTED_EDGE ( 'NONE', *, *, #92201, .F. ) ;
#5003=EDGE_LOOP ( 'NONE', ( #39447, #76144, #93489, #83106, #65818 ) ) ;
#5070=CARTESIAN_POINT ( 'NONE',  ( -0.3244794670026781014, -9.612687562450236811, -9.000000000000000000 ) ) ;
#5181=ORIENTED_EDGE ( 'NONE', *, *, #40669, .F. ) ;
#5361=CARTESIAN_POINT ( 'NONE',  ( -2.717543299849222826, 17.80004702990586196, -9.000000000000000000 ) ) ;
#5550=CIRCLE ( 'NONE', #53940, 10.11363636363636154 ) ;
#5565=CARTESIAN_POINT ( 'NONE',  ( -3.302878749216429544, 14.80319218833827044, 8.673617379884035472E-16 ) ) ;
#5623=VERTEX_POINT ( 'NONE', #99583 ) ;
#5758=AXIS2_PLACEMENT_3D ( 'NONE', #87249, #49713, #32975 ) ;
#5767=ORIENTED_EDGE ( 'NONE', *, *, #41579, .F. ) ;
#5768=ORIENTED_EDGE ( 'NONE', *, *, #49672, .F. ) ;
#5771=EDGE_LOOP ( 'NONE', ( #63225, #25539, #46611, #71942 ) ) ;
#5816=CARTESIAN_POINT ( 'NONE',  ( -3.388261204761456646, -14.20760230196127516, 0.000000000000000000 ) ) ;
#5922=VERTEX_POINT ( 'NONE', #19367 ) ;
#5941=LINE ( 'NONE', #14550, #63461 ) ;
#5962=DIRECTION ( 'NONE',  ( 0.06975647374412546897, 0.9975640502598241977, 4.700301109882544451E-17 ) ) ;
#5975=DIRECTION ( 'NONE',  ( -0.000000000000000000, -0.000000000000000000, -1.000000000000000000 ) ) ;
#6117=ADVANCED_FACE ( 'NONE', ( #32867 ), #55217, .T. ) ;
#6185=EDGE_CURVE ( 'NONE', #98585, #92378, #17332, .T. ) ;
#6226=CYLINDRICAL_SURFACE ( 'NONE', #38811, 2.499999999999963141 ) ;
#6245=CARTESIAN_POINT ( 'NONE',  ( -0.3244794670026783234, -9.612687562450236811, 9.000000000000000000 ) ) ;
#6302=DIRECTION ( 'NONE',  ( 0.2164396139380966033, -0.9762960071199348056, 4.401934094135205585E-16 ) ) ;
#6334=DESIGN_CONTEXT ( 'detailed design', #97813, 'design' ) ;
#6373=ORIENTED_EDGE ( 'NONE', *, *, #14607, .T. ) ;
#6431=PLANE ( 'NONE',  #31210 ) ;
#6432=CARTESIAN_POINT ( 'NONE',  ( 1.259127588940877285, 10.83856991095998801, 0.000000000000000000 ) ) ;
#6516=VECTOR ( 'NONE', #31073, 1000.000000000000000 ) ;
#6558=DIRECTION ( 'NONE',  ( -1.000000000000000000, 0.000000000000000000, -3.469446951953617147E-16 ) ) ;
#6703=ORIENTED_EDGE ( 'NONE', *, *, #91341, .T. ) ;
#6721=ORIENTED_EDGE ( 'NONE', *, *, #85622, .T. ) ;
#6799=EDGE_CURVE ( 'NONE', #1781, #89454, #56110, .T. ) ;
#7102=AXIS2_PLACEMENT_3D ( 'NONE', #46134, #98902, #100385 ) ;
#7375=LINE ( 'NONE', #86006, #87349 ) ;
#7466=LINE ( 'NONE', #31310, #82493 ) ;
#7502=ORIENTED_EDGE ( 'NONE', *, *, #9009, .T. ) ;
#7510=EDGE_LOOP ( 'NONE', ( #52672, #41872, #14007, #28461 ) ) ;
#7666=AXIS2_PLACEMENT_3D ( 'NONE', #16403, #77793, #47374 ) ;
#7676=LINE ( 'NONE', #99506, #87970 ) ;
#7717=APPLICATION_CONTEXT ( 'configuration controlled 3d designs of mechanical parts and assemblies' ) ;
#7839=CIRCLE ( 'NONE', #74344, 3.549999999999999378 ) ;
#8095=CARTESIAN_POINT ( 'NONE',  ( 0.1334620785917008390, -8.769264156269322541, -9.000000000000000000 ) ) ;
#8186=LINE ( 'NONE', #32523, #41553 ) ;
#8242=DIRECTION ( 'NONE',  ( -0.4771587602595986910, -0.8788171126619707119, 0.000000000000000000 ) ) ;
#8300=DIRECTION ( 'NONE',  ( 0.000000000000000000, 0.000000000000000000, -1.000000000000000000 ) ) ;
#8345=ORIENTED_EDGE ( 'NONE', *, *, #35271, .F. ) ;
#8415=ORIENTED_EDGE ( 'NONE', *, *, #23300, .F. ) ;
#8834=DIRECTION ( 'NONE',  ( 0.9975640502598247528, -0.06975647374411753088, 0.000000000000000000 ) ) ;
#8876=ORIENTED_EDGE ( 'NONE', *, *, #58380, .T. ) ;
#8961=ORIENTED_EDGE ( 'NONE', *, *, #55002, .F. ) ;
#9009=EDGE_CURVE ( 'NONE', #52065, #67869, #49617, .T. ) ;
#9052=VECTOR ( 'NONE', #62013, 1000.000000000000000 ) ;
#9108=ORIENTED_EDGE ( 'NONE', *, *, #90095, .T. ) ;
#9246=VECTOR ( 'NONE', #66214, 1000.000000000000114 ) ;
#9338=DIRECTION ( 'NONE',  ( 0.000000000000000000, 0.000000000000000000, 1.000000000000000000 ) ) ;
#9438=DIRECTION ( 'NONE',  ( -0.8788171126619707119, 0.4771587602595986910, 0.000000000000000000 ) ) ;
#9530=ORIENTED_EDGE ( 'NONE', *, *, #73942, .F. ) ;
#9643=AXIS2_PLACEMENT_3D ( 'NONE', #9645, #64967, #64469 ) ;
#9645=CARTESIAN_POINT ( 'NONE',  ( 0.7603455638109648529, 10.87344814783205038, 0.000000000000000000 ) ) ;
#9851=VECTOR ( 'NONE', #78242, 1000.000000000000000 ) ;
#10069=ORIENTED_EDGE ( 'NONE', *, *, #67137, .T. ) ;
#10084=PLANE ( 'NONE',  #70733 ) ;
#10134=DIRECTION ( 'NONE',  ( 0.1478094111296165969, -0.9890158633619159367, 0.000000000000000000 ) ) ;
#10138=EDGE_CURVE ( 'NONE', #25637, #81283, #7676, .T. ) ;
#10173=MANIFOLD_SOLID_BREP ( 'Kes-Ekstr\X2\00fc\X0\zyon2', #87320 ) ;
#10189=DIRECTION ( 'NONE',  ( 0.06975647374412546897, 0.9975640502598241977, 0.000000000000000000 ) ) ;
#10259=CARTESIAN_POINT ( 'NONE',  ( 3.138110291115776995, 11.54688212118755075, 3.549999999999999822 ) ) ;
#10708=ORIENTED_EDGE ( 'NONE', *, *, #27874, .T. ) ;
#10745=CIRCLE ( 'NONE', #20431, 5.500000000000001776 ) ;
#10853=VECTOR ( 'NONE', #96492, 1000.000000000000114 ) ;
#10903=CIRCLE ( 'NONE', #22246, 2.899999999999999467 ) ;
#10958=CARTESIAN_POINT ( 'NONE',  ( 0.2450472757604422180, -5.405843919193447533, 9.000000000000000000 ) ) ;
#11106=ORIENTED_EDGE ( 'NONE', *, *, #74234, .F. ) ;
#11180=CARTESIAN_POINT ( 'NONE',  ( 0.2746452767749877344, 3.927610442141366676, 1.700000000000008615 ) ) ;
#11302=CIRCLE ( 'NONE', #51793, 21.24999999999998934 ) ;
#11393=ADVANCED_FACE ( 'NONE', ( #35652 ), #90925, .F. ) ;
#11394=AXIS2_PLACEMENT_3D ( 'NONE', #31829, #63804, #46553 ) ;
#11447=LINE ( 'NONE', #19055, #20265 ) ;
#11453=VECTOR ( 'NONE', #16909, 1000.000000000000000 ) ;
#11484=LINE ( 'NONE', #49068, #90002 ) ;
#11560=ADVANCED_FACE ( 'NONE', ( #54759 ), #16677, .F. ) ;
#11660=CIRCLE ( 'NONE', #40860, 3.549999999999999378 ) ;
#11677=LINE ( 'NONE', #3098, #49052 ) ;
#11943=DIRECTION ( 'NONE',  ( 1.084136044942898696E-16, 0.000000000000000000, -1.000000000000000000 ) ) ;
#11975=LINE ( 'NONE', #26706, #77146 ) ;
#12035=CARTESIAN_POINT ( 'NONE',  ( -1.675486951385420475, 10.82748519320431591, 3.549999999999999822 ) ) ;
#12078=EDGE_CURVE ( 'NONE', #14465, #39424, #11447, .T. ) ;
#12105=VERTEX_POINT ( 'NONE', #80964 ) ;
#12160=DIRECTION ( 'NONE',  ( 0.9975640502598241977, -0.06975647374412546897, -0.000000000000000000 ) ) ;
#12261=AXIS2_PLACEMENT_3D ( 'NONE', #77551, #83675, #6558 ) ;
#12523=ORIENTED_EDGE ( 'NONE', *, *, #16995, .T. ) ;
#12525=CIRCLE ( 'NONE', #59535, 2.899999999999999467 ) ;
#12612=VECTOR ( 'NONE', #58622, 1000.000000000000114 ) ;
#12629=AXIS2_PLACEMENT_3D ( 'NONE', #24093, #70284, #76867 ) ;
#12674=LINE ( 'NONE', #4584, #77993 ) ;
#12812=CARTESIAN_POINT ( 'NONE',  ( -3.212051231530181017, 17.72614232434105475, 8.999999999999998224 ) ) ;
#12831=CARTESIAN_POINT ( 'NONE',  ( 0.7395552074414002419, -5.331939213628640317, 8.999999999999998224 ) ) ;
#13322=EDGE_CURVE ( 'NONE', #25637, #58202, #18204, .T. ) ;
#13404=DIRECTION ( 'NONE',  ( -0.9762960071199348056, -0.2164396139380966033, -3.469446951953617147E-16 ) ) ;
#13464=EDGE_CURVE ( 'NONE', #45390, #74792, #81922, .T. ) ;
#13525=CARTESIAN_POINT ( 'NONE',  ( 0.7603455638109648529, 10.87344814783205038, 0.000000000000000000 ) ) ;
#13553=FACE_OUTER_BOUND ( 'NONE', #4163, .T. ) ;
#13572=VERTEX_POINT ( 'NONE', #59652 ) ;
#13658=ORIENTED_EDGE ( 'NONE', *, *, #18155, .T. ) ;
#13713=AXIS2_PLACEMENT_3D ( 'NONE', #73049, #65452, #36464 ) ;
#13809=CARTESIAN_POINT ( 'NONE',  ( -1.164890887384984586, 4.028272616778474813, -2.677392948487098267E-15 ) ) ;
#13935=CIRCLE ( 'NONE', #99822, 9.999999999999991118 ) ;
#13943=CARTESIAN_POINT ( 'NONE',  ( 0.3244565263465142291, -1.558659884777352067, -8.999999999999998224 ) ) ;
#13953=AXIS2_PLACEMENT_3D ( 'NONE', #76394, #37849, #23101 ) ;
#14007=ORIENTED_EDGE ( 'NONE', *, *, #89409, .F. ) ;
#14165=DIRECTION ( 'NONE',  ( -0.2164396139380965756, 0.9762960071199346945, 0.000000000000000000 ) ) ;
#14167=EDGE_CURVE ( 'NONE', #2990, #74103, #31046, .T. ) ;
#14177=ORIENTED_EDGE ( 'NONE', *, *, #31922, .T. ) ;
#14191=DIRECTION ( 'NONE',  ( 0.1478094111296165969, -0.9890158633619159367, 0.000000000000000000 ) ) ;
#14395=FACE_BOUND ( 'NONE', #89140, .T. ) ;
#14402=VECTOR ( 'NONE', #16767, 1000.000000000000114 ) ;
#14465=VERTEX_POINT ( 'NONE', #45179 ) ;
#14528=DIRECTION ( 'NONE',  ( 0.9975640502598241977, -0.06975647374412546897, -0.000000000000000000 ) ) ;
#14550=CARTESIAN_POINT ( 'NONE',  ( 0.8635838190919263857, -3.990505948720460605, -8.999999999999998224 ) ) ;
#14607=EDGE_CURVE ( 'NONE', #1549, #89739, #40061, .T. ) ;
#14765=( GEOMETRIC_REPRESENTATION_CONTEXT ( 3 ) GLOBAL_UNCERTAINTY_ASSIGNED_CONTEXT ( ( #73365 ) ) GLOBAL_UNIT_ASSIGNED_CONTEXT ( ( #89951, #63274, #66650 ) ) REPRESENTATION_CONTEXT ( 'NONE', 'WORKASPACE' ) );
#14827=AXIS2_PLACEMENT_3D ( 'NONE', #50885, #29024, #82318 ) ;
#14860=DIRECTION ( 'NONE',  ( -4.335561085774420994E-16, -0.000000000000000000, 1.000000000000000000 ) ) ;
#14893=FACE_OUTER_BOUND ( 'NONE', #33612, .T. ) ;
#14927=DIRECTION ( 'NONE',  ( -0.000000000000000000, -0.000000000000000000, -1.000000000000000000 ) ) ;
#14983=CARTESIAN_POINT ( 'NONE',  ( 0.7734273019049007214, 3.892732205269316292, -2.677392948487098267E-15 ) ) ;
#15228=EDGE_LOOP ( 'NONE', ( #31010, #3310, #93741, #66167 ) ) ;
#15450=ORIENTED_EDGE ( 'NONE', *, *, #38383, .F. ) ;
#15490=ORIENTED_EDGE ( 'NONE', *, *, #64608, .F. ) ;
#15594=ORIENTED_EDGE ( 'NONE', *, *, #87958, .T. ) ;
#15691=EDGE_CURVE ( 'NONE', #92378, #47484, #91424, .T. ) ;
#15701=FACE_OUTER_BOUND ( 'NONE', #37836, .T. ) ;
#16070=VECTOR ( 'NONE', #40510, 1000.000000000000000 ) ;
#16092=ORIENTED_EDGE ( 'NONE', *, *, #91341, .F. ) ;
#16155=VECTOR ( 'NONE', #20011, 1000.000000000000114 ) ;
#16260=EDGE_LOOP ( 'NONE', ( #57470, #89751, #67072, #55580 ) ) ;
#16272=LINE ( 'NONE', #85276, #14402 ) ;
#16364=AXIS2_PLACEMENT_3D ( 'NONE', #33267, #64255, #34781 ) ;
#16401=VERTEX_POINT ( 'NONE', #64909 ) ;
#16403=CARTESIAN_POINT ( 'NONE',  ( 0.2746452767749879009, 3.927610442141378666, -2.677392948487098267E-15 ) ) ;
#16425=LINE ( 'NONE', #61635, #43626 ) ;
#16487=VERTEX_POINT ( 'NONE', #20185 ) ;
#16568=EDGE_CURVE ( 'NONE', #97920, #89739, #61769, .T. ) ;
#16677=PLANE ( 'NONE',  #75241 ) ;
#16767=DIRECTION ( 'NONE',  ( -0.9975640502598241977, 0.06975647374412534407, 3.469446951953616654E-16 ) ) ;
#16782=CARTESIAN_POINT ( 'NONE',  ( -3.212051231530180573, 17.72614232434105119, -9.000000000000000000 ) ) ;
#16909=DIRECTION ( 'NONE',  ( -0.9762960071199348056, -0.2164396139380966033, 6.123031769111886291E-17 ) ) ;
#16937=ORIENTED_EDGE ( 'NONE', *, *, #17846, .T. ) ;
#16967=DIRECTION ( 'NONE',  ( 1.084136044942898696E-16, 0.000000000000000000, -1.000000000000000000 ) ) ;
#16995=EDGE_CURVE ( 'NONE', #43562, #76018, #30037, .T. ) ;
#17051=DIRECTION ( 'NONE',  ( -0.4771587602595986910, -0.8788171126619707119, 0.000000000000000000 ) ) ;
#17057=DIRECTION ( 'NONE',  ( -1.000000000000000000, 0.000000000000000000, 0.000000000000000000 ) ) ;
#17201=DIRECTION ( 'NONE',  ( 9.426781450619601849E-18, -6.307606751056558338E-17, 1.000000000000000000 ) ) ;
#17272=DIRECTION ( 'NONE',  ( -1.000000000000000000, 0.000000000000000000, -0.000000000000000000 ) ) ;
#17295=DIRECTION ( 'NONE',  ( 4.335561085774420994E-16, 0.000000000000000000, -1.000000000000000000 ) ) ;
#17332=CIRCLE ( 'NONE', #23779, 1.999999999999963141 ) ;
#17557=CARTESIAN_POINT ( 'NONE',  ( 1.876957540558651605, -5.558144974487054135, 0.000000000000000000 ) ) ;
#17645=DIRECTION ( 'NONE',  ( -0.4771587602595986910, -0.8788171126619707119, 0.000000000000000000 ) ) ;
#17652=PLANE ( 'NONE',  #28720 ) ;
#17697=EDGE_LOOP ( 'NONE', ( #16092, #48695, #33482, #99286, #73400 ) ) ;
#17731=CARTESIAN_POINT ( 'NONE',  ( 0.5999240985075944277, 1.411520799013914917, -8.999999999999994671 ) ) ;
#17750=FACE_OUTER_BOUND ( 'NONE', #62933, .T. ) ;
#17766=AXIS2_PLACEMENT_3D ( 'NONE', #29055, #98559, #59028 ) ;
#17791=LINE ( 'NONE', #24889, #69343 ) ;
#17799=ORIENTED_EDGE ( 'NONE', *, *, #88894, .T. ) ;
#17823=VECTOR ( 'NONE', #83364, 1000.000000000000114 ) ;
#17846=EDGE_CURVE ( 'NONE', #81283, #67869, #10745, .T. ) ;
#17850=DIRECTION ( 'NONE',  ( -0.9762960071199348056, -0.2164396139380966033, -0.000000000000000000 ) ) ;
#17858=VERTEX_POINT ( 'NONE', #90220 ) ;
#17896=DIRECTION ( 'NONE',  ( 4.335561085774420994E-16, 0.000000000000000000, -1.000000000000000000 ) ) ;
#17902=VECTOR ( 'NONE', #66353, 1000.000000000000114 ) ;
#18064=DIRECTION ( 'NONE',  ( -0.000000000000000000, -0.000000000000000000, -1.000000000000000000 ) ) ;
#18136=DIRECTION ( 'NONE',  ( -0.8788171126619707119, 0.4771587602595986910, -0.000000000000000000 ) ) ;
#18155=EDGE_CURVE ( 'NONE', #89454, #92378, #11975, .T. ) ;
#18204=LINE ( 'NONE', #97198, #80323 ) ;
#18314=ORIENTED_EDGE ( 'NONE', *, *, #99023, .T. ) ;
#18415=CIRCLE ( 'NONE', #63786, 21.24999999999998579 ) ;
#18635=CARTESIAN_POINT ( 'NONE',  ( 1.876957540558651605, -5.558144974487054135, 0.000000000000000000 ) ) ;
#18660=DIRECTION ( 'NONE',  ( -0.9890158633619159367, -0.1478094111296165969, 0.000000000000000000 ) ) ;
#18856=VERTEX_POINT ( 'NONE', #5070 ) ;
#18896=FACE_OUTER_BOUND ( 'NONE', #83103, .T. ) ;
#18988=EDGE_LOOP ( 'NONE', ( #5181, #92852, #13658, #62670 ) ) ;
#19005=LINE ( 'NONE', #72812, #9246 ) ;
#19055=CARTESIAN_POINT ( 'NONE',  ( 0.5964549592197745387, 8.529703308962702124, 1.700000000000008837 ) ) ;
#19367=CARTESIAN_POINT ( 'NONE',  ( 0.7734273019049007214, 3.892732205269316292, 1.700000000000006839 ) ) ;
#19446=FACE_OUTER_BOUND ( 'NONE', #45459, .T. ) ;
#19453=EDGE_LOOP ( 'NONE', ( #99635, #71137, #81429, #88868 ) ) ;
#19552=CARTESIAN_POINT ( 'NONE',  ( 0.3244565263465140070, -1.558659884777350735, 2.575303280952439950E-15 ) ) ;
#19708=VERTEX_POINT ( 'NONE', #79609 ) ;
#19943=CYLINDRICAL_SURFACE ( 'NONE', #17766, 2.899999999999999467 ) ;
#20011=DIRECTION ( 'NONE',  ( -0.9890158633619158257, -0.1478094111296165691, -0.000000000000000000 ) ) ;
#20185=CARTESIAN_POINT ( 'NONE',  ( 0.1011420733776737524, 1.446399035885977957, 8.999999999999987566 ) ) ;
#20201=CARTESIAN_POINT ( 'NONE',  ( -0.3244794670026783234, -9.612687562450236811, 9.000000000000000000 ) ) ;
#20265=VECTOR ( 'NONE', #49530, 1000.000000000000114 ) ;
#20333=ORIENTED_EDGE ( 'NONE', *, *, #28592, .T. ) ;
#20422=AXIS2_PLACEMENT_3D ( 'NONE', #50636, #89698, #28792 ) ;
#20431=AXIS2_PLACEMENT_3D ( 'NONE', #3992, #5975, #90717 ) ;
#20610=ORIENTED_EDGE ( 'NONE', *, *, #71317, .F. ) ;
#20700=LINE ( 'NONE', #20201, #60612 ) ;
#20784=AXIS2_PLACEMENT_3D ( 'NONE', #64902, #95811, #26310 ) ;
#20943=CARTESIAN_POINT ( 'NONE',  ( 10.57556460110582996, 0.7139560615726621151, -8.999999999999991118 ) ) ;
#21305=ORIENTED_EDGE ( 'NONE', *, *, #74947, .T. ) ;
#21357=EDGE_CURVE ( 'NONE', #5922, #97920, #41763, .T. ) ;
#21412=DIRECTION ( 'NONE',  ( 1.000000000000000000, 0.000000000000000000, 0.000000000000000000 ) ) ;
#21529=CARTESIAN_POINT ( 'NONE',  ( 0.2746452767749879009, 3.927610442141378666, -1.700000000000009059 ) ) ;
#21554=DIRECTION ( 'NONE',  ( 0.1478094111296165969, -0.9890158633619159367, 0.000000000000000000 ) ) ;
#21589=ORIENTED_EDGE ( 'NONE', *, *, #39354, .F. ) ;
#21849=LINE ( 'NONE', #51328, #50146 ) ;
#22246=AXIS2_PLACEMENT_3D ( 'NONE', #57357, #3060, #34502 ) ;
#22275=CIRCLE ( 'NONE', #79002, 10.11363636363636331 ) ;
#22416=DIRECTION ( 'NONE',  ( -0.2164396139380966033, 0.9762960071199348056, -0.000000000000000000 ) ) ;
#22448=AXIS2_PLACEMENT_3D ( 'NONE', #79599, #62387, #55788 ) ;
#23101=DIRECTION ( 'NONE',  ( 1.000000000000000000, 0.000000000000000000, 0.000000000000000000 ) ) ;
#23148=DIRECTION ( 'NONE',  ( -0.000000000000000000, -0.000000000000000000, 1.000000000000000000 ) ) ;
#23300=EDGE_CURVE ( 'NONE', #58202, #47484, #96502, .T. ) ;
#23589=EDGE_LOOP ( 'NONE', ( #7502, #4862, #10069, #79369 ) ) ;
#23680=EDGE_CURVE ( 'NONE', #41863, #5922, #33452, .T. ) ;
#23779=AXIS2_PLACEMENT_3D ( 'NONE', #84521, #69301, #76889 ) ;
#23968=LINE ( 'NONE', #69151, #69114 ) ;
#24009=CARTESIAN_POINT ( 'NONE',  ( 0.4987820251299121543, -0.03487823687206273449, 9.000000000000000000 ) ) ;
#24085=DIRECTION ( 'NONE',  ( 0.000000000000000000, 0.000000000000000000, -1.000000000000000000 ) ) ;
#24093=CARTESIAN_POINT ( 'NONE',  ( 4.143214286797170409, 4.821574250326516875, -2.677392948487098267E-15 ) ) ;
#24228=ORIENTED_EDGE ( 'NONE', *, *, #61709, .T. ) ;
#24274=AXIS2_PLACEMENT_3D ( 'NONE', #71313, #55595, #86524 ) ;
#24459=VERTEX_POINT ( 'NONE', #43830 ) ;
#24581=ORIENTED_EDGE ( 'NONE', *, *, #92283, .F. ) ;
#24623=ORIENTED_EDGE ( 'NONE', *, *, #14607, .F. ) ;
#24759=ORIENTED_EDGE ( 'NONE', *, *, #99948, .F. ) ;
#24785=CARTESIAN_POINT ( 'NONE',  ( 0.9317375178030620209, -7.299023693294228288, -9.000000000000000000 ) ) ;
#24845=VECTOR ( 'NONE', #18064, 1000.000000000000000 ) ;
#24854=DIRECTION ( 'NONE',  ( 1.000000000000000000, 0.000000000000000000, 0.000000000000000000 ) ) ;
#24889=CARTESIAN_POINT ( 'NONE',  ( 0.5999240985075944277, 1.411520799013914917, -8.999999999999998224 ) ) ;
#25021=EDGE_CURVE ( 'NONE', #51300, #82863, #89882, .T. ) ;
#25150=CARTESIAN_POINT ( 'NONE',  ( 4.143214286797170409, 4.821574250326516875, -2.677392948487098267E-15 ) ) ;
#25294=DIRECTION ( 'NONE',  ( 0.000000000000000000, 0.000000000000000000, 1.000000000000000000 ) ) ;
#25426=DIRECTION ( 'NONE',  ( 0.1478094111296165691, -0.9890158633619158257, 0.000000000000000000 ) ) ;
#25504=CARTESIAN_POINT ( 'NONE',  ( 10.57556460110582996, 0.7139560615726621151, -8.999999999999994671 ) ) ;
#25508=EDGE_CURVE ( 'NONE', #45390, #59310, #19005, .T. ) ;
#25539=ORIENTED_EDGE ( 'NONE', *, *, #67636, .F. ) ;
#25637=VERTEX_POINT ( 'NONE', #52964 ) ;
#25761=AXIS2_PLACEMENT_3D ( 'NONE', #28173, #59132, #83946 ) ;
#25800=DIRECTION ( 'NONE',  ( 0.8788171126619707119, -0.4771587602595987465, 0.000000000000000000 ) ) ;
#26026=ORIENTED_EDGE ( 'NONE', *, *, #41579, .T. ) ;
#26029=CARTESIAN_POINT ( 'NONE',  ( 0.8126045299064811323, -1.450440077808301975, 8.999999999999998224 ) ) ;
#26101=DIRECTION ( 'NONE',  ( 1.000000000000000000, 0.000000000000000000, 1.084136044942898696E-16 ) ) ;
#26111=PLANE ( 'NONE',  #32934 ) ;
#26209=VECTOR ( 'NONE', #23148, 1000.000000000000000 ) ;
#26212=ADVANCED_FACE ( 'NONE', ( #54345 ), #46728, .F. ) ;
#26232=AXIS2_PLACEMENT_3D ( 'NONE', #98416, #43164, #28919 ) ;
#26252=DIRECTION ( 'NONE',  ( -0.4771587602595986910, -0.8788171126619707119, 0.000000000000000000 ) ) ;
#26310=DIRECTION ( 'NONE',  ( 0.06975647374412549673, 0.9975640502598241977, 0.000000000000000000 ) ) ;
#26338=PRODUCT_DEFINITION_SHAPE ( 'NONE', 'NONE',  #95340 ) ;
#26418=VERTEX_POINT ( 'NONE', #87017 ) ;
#26679=LINE ( 'NONE', #57144, #66856 ) ;
#26706=CARTESIAN_POINT ( 'NONE',  ( 0.000000000000000000, 0.000000000000000000, -9.000000000000000000 ) ) ;
#26907=AXIS2_PLACEMENT_3D ( 'NONE', #25504, #17896, #48858 ) ;
#27112=EDGE_CURVE ( 'NONE', #2990, #18856, #22275, .T. ) ;
#27267=EDGE_LOOP ( 'NONE', ( #45591, #86405, #6703, #1138 ) ) ;
#27331=DIRECTION ( 'NONE',  ( -0.4771587602595988020, -0.8788171126619706008, -0.000000000000000000 ) ) ;
#27654=FACE_OUTER_BOUND ( 'NONE', #74310, .T. ) ;
#27697=DIRECTION ( 'NONE',  ( -0.1478094111296165691, 0.9890158633619158257, -0.000000000000000000 ) ) ;
#27855=PLANE ( 'NONE',  #13713 ) ;
#27874=EDGE_CURVE ( 'NONE', #74792, #64635, #77255, .T. ) ;
#27883=LINE ( 'NONE', #58840, #66969 ) ;
#27928=EDGE_LOOP ( 'NONE', ( #89371, #91473, #14177, #20610 ) ) ;
#27956=CARTESIAN_POINT ( 'NONE',  ( 1.255616527394258553, 17.95615290467683778, -9.000000000000000000 ) ) ;
#28022=LINE ( 'NONE', #50368, #93449 ) ;
#28034=LINE ( 'NONE', #67112, #61784 ) ;
#28060=DIRECTION ( 'NONE',  ( 0.1478094111296165969, -0.9890158633619159367, 0.000000000000000000 ) ) ;
#28173=CARTESIAN_POINT ( 'NONE',  ( 0.8635838190919263857, -3.990505948720460605, -8.999999999999998224 ) ) ;
#28461=ORIENTED_EDGE ( 'NONE', *, *, #38465, .F. ) ;
#28486=VERTEX_POINT ( 'NONE', #29262 ) ;
#28568=FACE_OUTER_BOUND ( 'NONE', #27928, .T. ) ;
#28592=EDGE_CURVE ( 'NONE', #89739, #24459, #12525, .T. ) ;
#28720=AXIS2_PLACEMENT_3D ( 'NONE', #86659, #87162, #80050 ) ;
#28785=AXIS2_PLACEMENT_3D ( 'NONE', #42758, #73691, #49877 ) ;
#28792=DIRECTION ( 'NONE',  ( -0.2164396139380966033, 0.9762960071199348056, 0.000000000000000000 ) ) ;
#28919=DIRECTION ( 'NONE',  ( 0.1478094111296165969, -0.9890158633619159367, 0.000000000000000000 ) ) ;
#28959=ORIENTED_EDGE ( 'NONE', *, *, #54883, .T. ) ;
#29024=DIRECTION ( 'NONE',  ( -0.8788171126619707119, 0.4771587602595986910, 0.000000000000000000 ) ) ;
#29055=CARTESIAN_POINT ( 'NONE',  ( -4.045674540461745572, 11.20951781186025897, 0.000000000000000000 ) ) ;
#29196=EDGE_CURVE ( 'NONE', #39424, #85639, #51423, .T. ) ;
#29262=CARTESIAN_POINT ( 'NONE',  ( -0.7638880233336636794, -9.374108182320437521, 9.000000000000000000 ) ) ;
#29359=FACE_BOUND ( 'NONE', #35980, .T. ) ;
#29375=LINE ( 'NONE', #98379, #88031 ) ;
#29617=ORIENTED_EDGE ( 'NONE', *, *, #30266, .F. ) ;
#29853=VERTEX_POINT ( 'NONE', #60871 ) ;
#30000=VECTOR ( 'NONE', #94836, 1000.000000000000114 ) ;
#30037=LINE ( 'NONE', #39158, #38049 ) ;
#30117=ORIENTED_EDGE ( 'NONE', *, *, #13464, .T. ) ;
#30266=EDGE_CURVE ( 'NONE', #52789, #40572, #43177, .T. ) ;
#30502=CARTESIAN_POINT ( 'NONE',  ( 0.7395552074414004640, -5.331939213628641205, -9.000000000000000000 ) ) ;
#30653=LINE ( 'NONE', #1211, #66669 ) ;
#30771=AXIS2_PLACEMENT_3D ( 'NONE', #80347, #88469, #80855 ) ;
#30882=EDGE_CURVE ( 'NONE', #64635, #75345, #80826, .T. ) ;
#30994=EDGE_CURVE ( 'NONE', #82528, #19708, #48883, .T. ) ;
#31010=ORIENTED_EDGE ( 'NONE', *, *, #14167, .F. ) ;
#31022=EDGE_CURVE ( 'NONE', #16401, #78060, #28034, .T. ) ;
#31046=LINE ( 'NONE', #71127, #9052 ) ;
#31073=DIRECTION ( 'NONE',  ( -0.8788171126619707119, 0.4771587602595986910, -0.000000000000000000 ) ) ;
#31210=AXIS2_PLACEMENT_3D ( 'NONE', #92649, #45504, #93146 ) ;
#31310=CARTESIAN_POINT ( 'NONE',  ( 0.8126045299064816874, -1.450440077808303752, -8.999999999999998224 ) ) ;
#31526=EDGE_CURVE ( 'NONE', #1781, #16401, #5941, .T. ) ;
#31550=DIRECTION ( 'NONE',  ( -0.000000000000000000, 0.000000000000000000, -1.000000000000000000 ) ) ;
#31566=EDGE_CURVE ( 'NONE', #58202, #42138, #36398, .T. ) ;
#31680=CARTESIAN_POINT ( 'NONE',  ( -4.700032041049139409, -6.144890974841530351, 9.000000000000000000 ) ) ;
#31725=AXIS2_PLACEMENT_3D ( 'NONE', #84957, #53035, #21554 ) ;
#31829=CARTESIAN_POINT ( 'NONE',  ( -1.877194073982709988, 8.794404527355018431, 0.000000000000000000 ) ) ;
#31922=EDGE_CURVE ( 'NONE', #1781, #76018, #43410, .T. ) ;
#31934=PLANE ( 'NONE',  #80794 ) ;
#31992=CARTESIAN_POINT ( 'NONE',  ( 4.667937696307308926, 1.310567935391715899, -2.677392948487098267E-15 ) ) ;
#32083=ORIENTED_EDGE ( 'NONE', *, *, #6185, .F. ) ;
#32142=CARTESIAN_POINT ( 'NONE',  ( 0.2450472757604428842, -5.405843919193451086, 9.000000000000000000 ) ) ;
#32192=DIRECTION ( 'NONE',  ( 0.9762960071199348056, 0.2164396139380966033, 0.000000000000000000 ) ) ;
#32523=CARTESIAN_POINT ( 'NONE',  ( 0.000000000000000000, 0.000000000000000000, 9.000000000000000000 ) ) ;
#32564=DIRECTION ( 'NONE',  ( 0.4771587602595988020, 0.8788171126619706008, -0.000000000000000000 ) ) ;
#32803=SHAPE_REPRESENTATION_RELATIONSHIP ( 'NONE' , 'NONE' ,  #36681, #67027 ) ;
#32863=ORIENTED_EDGE ( 'NONE', *, *, #59817, .T. ) ;
#32867=FACE_OUTER_BOUND ( 'NONE', #15228, .T. ) ;
#32933=CARTESIAN_POINT ( 'NONE',  ( -0.6703829557040261733, 4.102177322343280252, -3.549999999999999378 ) ) ;
#32934=AXIS2_PLACEMENT_3D ( 'NONE', #71794, #49466, #2289 ) ;
#32975=DIRECTION ( 'NONE',  ( -1.000000000000000000, 0.000000000000000000, 0.000000000000000000 ) ) ;
#33028=CARTESIAN_POINT ( 'NONE',  ( 1.255616527394258553, 17.95615290467683778, 9.000000000000000000 ) ) ;
#33191=CARTESIAN_POINT ( 'NONE',  ( 0.000000000000000000, 0.000000000000000000, 9.000000000000000000 ) ) ;
#33267=CARTESIAN_POINT ( 'NONE',  ( -4.700032041049139409, -6.144890974841530351, -9.000000000000000000 ) ) ;
#33357=CIRCLE ( 'NONE', #4179, 2.499999999999963141 ) ;
#33405=FACE_OUTER_BOUND ( 'NONE', #27267, .T. ) ;
#33407=AXIS2_PLACEMENT_3D ( 'NONE', #81590, #82082, #43032 ) ;
#33425=AXIS2_PLACEMENT_3D ( 'NONE', #5565, #83685, #14165 ) ;
#33452=LINE ( 'NONE', #48193, #90062 ) ;
#33482=ORIENTED_EDGE ( 'NONE', *, *, #42800, .T. ) ;
#33537=AXIS2_PLACEMENT_3D ( 'NONE', #98129, #58108, #51978 ) ;
#33612=EDGE_LOOP ( 'NONE', ( #95323, #91493, #69400, #15450 ) ) ;
#33625=ADVANCED_FACE ( 'NONE', ( #59025 ), #42316, .F. ) ;
#33713=DIRECTION ( 'NONE',  ( 0.1478094111296165691, -0.9890158633619158257, 0.000000000000000000 ) ) ;
#33738=ADVANCED_FACE ( 'NONE', ( #94454 ), #1619, .T. ) ;
#33872=EDGE_CURVE ( 'NONE', #70264, #82528, #66038, .T. ) ;
#33886=EDGE_LOOP ( 'NONE', ( #3516, #47688, #3405, #85596, #50816 ) ) ;
#33971=CARTESIAN_POINT ( 'NONE',  ( -0.3059464777392844059, -8.530684776139525027, -9.000000000000000000 ) ) ;
#34064=VECTOR ( 'NONE', #62924, 1000.000000000000000 ) ;
#34117=ORIENTED_EDGE ( 'NONE', *, *, #61709, .F. ) ;
#34347=CARTESIAN_POINT ( 'NONE',  ( -1.675486951385420475, 10.82748519320431591, 3.549999999999999822 ) ) ;
#34377=DIRECTION ( 'NONE',  ( 0.8788171126619707119, -0.4771587602595986910, 0.000000000000000000 ) ) ;
#34379=VECTOR ( 'NONE', #3445, 1000.000000000000000 ) ;
#34502=DIRECTION ( 'NONE',  ( -0.06975647374412549673, -0.9975640502598241977, 0.000000000000000000 ) ) ;
#34700=DIRECTION ( 'NONE',  ( -0.06975647374412546897, -0.9975640502598241977, 0.000000000000000000 ) ) ;
#34781=DIRECTION ( 'NONE',  ( 1.000000000000000000, 0.000000000000000000, 0.000000000000000000 ) ) ;
#35271=EDGE_CURVE ( 'NONE', #26418, #28486, #83867, .T. ) ;
#35408=CARTESIAN_POINT ( 'NONE',  ( 1.437548984227666304, -5.319565594357255733, 0.000000000000000000 ) ) ;
#35630=ORIENTED_EDGE ( 'NONE', *, *, #16568, .T. ) ;
#35652=FACE_OUTER_BOUND ( 'NONE', #90361, .T. ) ;
#35845=CARTESIAN_POINT ( 'NONE',  ( 1.754398552524098376, 17.92127466780477718, -9.000000000000000000 ) ) ;
#35905=FACE_OUTER_BOUND ( 'NONE', #7510, .T. ) ;
#35980=EDGE_LOOP ( 'NONE', ( #92225, #15490, #55907, #94388, #69676 ) ) ;
#36283=SHAPE_DEFINITION_REPRESENTATION ( #26338, #36681 ) ;
#36374=CARTESIAN_POINT ( 'NONE',  ( -0.3059464777392844059, -8.530684776139525027, 8.999999999999998224 ) ) ;
#36398=LINE ( 'NONE', #100263, #26209 ) ;
#36464=DIRECTION ( 'NONE',  ( 1.000000000000000000, 0.000000000000000000, 1.084136044942898696E-16 ) ) ;
#36564=EDGE_LOOP ( 'NONE', ( #82614, #91530, #69532, #59074 ) ) ;
#36638=DIRECTION ( 'NONE',  ( -4.335561085774420994E-16, -0.000000000000000000, 1.000000000000000000 ) ) ;
#36681=SHAPE_REPRESENTATION ( 'Tape Measure Hook', ( #37391 ), #14765 ) ;
#37140=FACE_OUTER_BOUND ( 'NONE', #5003, .T. ) ;
#37156=CARTESIAN_POINT ( 'NONE',  ( -4.700032041049139409, -6.144890974841530351, 8.999999999999998224 ) ) ;
#37182=DIRECTION ( 'NONE',  ( 1.084136044942898696E-16, 0.000000000000000000, -1.000000000000000000 ) ) ;
#37308=EDGE_CURVE ( 'NONE', #94609, #52065, #64349, .T. ) ;
#37388=VECTOR ( 'NONE', #6302, 1000.000000000000000 ) ;
#37391=AXIS2_PLACEMENT_3D ( 'NONE', #1533, #63447, #24854 ) ;
#37483=ORIENTED_EDGE ( 'NONE', *, *, #72761, .F. ) ;
#37602=ORIENTED_EDGE ( 'NONE', *, *, #87958, .F. ) ;
#37645=ORIENTED_EDGE ( 'NONE', *, *, #55894, .F. ) ;
#37688=DIRECTION ( 'NONE',  ( 0.8788171126619707119, -0.4771587602595986910, 0.000000000000000000 ) ) ;
#37749=CARTESIAN_POINT ( 'NONE',  ( 0.8126045299064811323, -1.450440077808301975, 8.999999999999998224 ) ) ;
#37836=EDGE_LOOP ( 'NONE', ( #48345, #40641, #91128, #41084 ) ) ;
#37849=DIRECTION ( 'NONE',  ( 0.000000000000000000, 0.000000000000000000, 1.000000000000000000 ) ) ;
#38049=VECTOR ( 'NONE', #22416, 1000.000000000000000 ) ;
#38320=DIRECTION ( 'NONE',  ( 0.06975647374412549673, 0.9975640502598241977, 0.000000000000000000 ) ) ;
#38383=EDGE_CURVE ( 'NONE', #29853, #5623, #29375, .T. ) ;
#38465=EDGE_CURVE ( 'NONE', #81283, #98585, #27883, .T. ) ;
#38811=AXIS2_PLACEMENT_3D ( 'NONE', #99553, #37182, #68138 ) ;
#39096=LINE ( 'NONE', #31992, #54654 ) ;
#39158=CARTESIAN_POINT ( 'NONE',  ( 0.01063402156994475850, -0.1430980438411110500, 9.000000000000000000 ) ) ;
#39228=ORIENTED_EDGE ( 'NONE', *, *, #77025, .T. ) ;
#39354=EDGE_CURVE ( 'NONE', #16401, #43562, #18415, .T. ) ;
#39393=FACE_OUTER_BOUND ( 'NONE', #17697, .T. ) ;
#39424=VERTEX_POINT ( 'NONE', #11180 ) ;
#39447=ORIENTED_EDGE ( 'NONE', *, *, #60215, .F. ) ;
#39638=ORIENTED_EDGE ( 'NONE', *, *, #72683, .T. ) ;
#39640=VECTOR ( 'NONE', #5962, 1000.000000000000227 ) ;
#39726=VECTOR ( 'NONE', #92964, 1000.000000000000000 ) ;
#39783=ORIENTED_EDGE ( 'NONE', *, *, #62995, .F. ) ;
#39935=FACE_OUTER_BOUND ( 'NONE', #77489, .T. ) ;
#39964=ORIENTED_EDGE ( 'NONE', *, *, #14167, .T. ) ;
#40054=EDGE_CURVE ( 'NONE', #28486, #74103, #45785, .T. ) ;
#40061=LINE ( 'NONE', #71015, #30000 ) ;
#40140=LINE ( 'NONE', #33028, #65084 ) ;
#40195=CARTESIAN_POINT ( 'NONE',  ( -0.3244794670026781014, -9.612687562450236811, -9.000000000000000000 ) ) ;
#40510=DIRECTION ( 'NONE',  ( -1.097118550003962868E-17, -2.020641003924594591E-17, -1.000000000000000000 ) ) ;
#40572=VERTEX_POINT ( 'NONE', #32142 ) ;
#40593=ORIENTED_EDGE ( 'NONE', *, *, #3104, .T. ) ;
#40641=ORIENTED_EDGE ( 'NONE', *, *, #21357, .T. ) ;
#40669=EDGE_CURVE ( 'NONE', #13572, #47484, #96434, .T. ) ;
#40694=ORIENTED_EDGE ( 'NONE', *, *, #61725, .T. ) ;
#40840=ORIENTED_EDGE ( 'NONE', *, *, #75642, .T. ) ;
#40860=AXIS2_PLACEMENT_3D ( 'NONE', #13809, #97560, #28060 ) ;
#41084=ORIENTED_EDGE ( 'NONE', *, *, #29196, .F. ) ;
#41135=CARTESIAN_POINT ( 'NONE',  ( 0.3244565263465140070, -1.558659884777350513, 8.999999999999978684 ) ) ;
#41553=VECTOR ( 'NONE', #10189, 1000.000000000000114 ) ;
#41579=EDGE_CURVE ( 'NONE', #40572, #25637, #64777, .T. ) ;
#41763=CIRCLE ( 'NONE', #98435, 1.700000000000008615 ) ;
#41854=FACE_OUTER_BOUND ( 'NONE', #36564, .T. ) ;
#41863=VERTEX_POINT ( 'NONE', #56021 ) ;
#41872=ORIENTED_EDGE ( 'NONE', *, *, #13322, .T. ) ;
#42006=CARTESIAN_POINT ( 'NONE',  ( -0.3059464777392852941, -8.530684776139525027, -9.000000000000000000 ) ) ;
#42096=VECTOR ( 'NONE', #57418, 1000.000000000000000 ) ;
#42138=VERTEX_POINT ( 'NONE', #12812 ) ;
#42162=EDGE_CURVE ( 'NONE', #39424, #5922, #75423, .T. ) ;
#42270=AXIS2_PLACEMENT_3D ( 'NONE', #79639, #72052, #10134 ) ;
#42316=PLANE ( 'NONE',  #30771 ) ;
#42428=DIRECTION ( 'NONE',  ( -0.000000000000000000, 0.000000000000000000, -1.000000000000000000 ) ) ;
#42758=CARTESIAN_POINT ( 'NONE',  ( 10.57556460110582286, 0.7139560615726621151, 8.999999999999994671 ) ) ;
#42800=EDGE_CURVE ( 'NONE', #26418, #2990, #3867, .T. ) ;
#42815=CYLINDRICAL_SURFACE ( 'NONE', #97884, 10.49999999999999289 ) ;
#42841=PLANE ( 'NONE',  #49455 ) ;
#42979=ORIENTED_EDGE ( 'NONE', *, *, #90095, .F. ) ;
#43032=DIRECTION ( 'NONE',  ( -0.1478094111296165691, 0.9890158633619158257, -0.000000000000000000 ) ) ;
#43164=DIRECTION ( 'NONE',  ( -0.9890158633619159367, -0.1478094111296165969, 0.000000000000000000 ) ) ;
#43177=CIRCLE ( 'NONE', #13953, 5.000000000000001776 ) ;
#43225=ORIENTED_EDGE ( 'NONE', *, *, #31566, .T. ) ;
#43410=LINE ( 'NONE', #19552, #74796 ) ;
#43442=DIRECTION ( 'NONE',  ( 0.06975647374412546897, 0.9975640502598241977, 0.000000000000000000 ) ) ;
#43562=VERTEX_POINT ( 'NONE', #72854 ) ;
#43626=VECTOR ( 'NONE', #14927, 1000.000000000000000 ) ;
#43797=VERTEX_POINT ( 'NONE', #62120 ) ;
#43830=CARTESIAN_POINT ( 'NONE',  ( 1.461421362798841272, 13.73150565671347678, 0.000000000000000000 ) ) ;
#43873=CYLINDRICAL_SURFACE ( 'NONE', #84379, 9.999999999999991118 ) ;
#44238=ORIENTED_EDGE ( 'NONE', *, *, #57989, .T. ) ;
#44249=DIRECTION ( 'NONE',  ( -0.9890158633619158257, -0.1478094111296165414, -0.000000000000000000 ) ) ;
#44533=EDGE_CURVE ( 'NONE', #12105, #69058, #67374, .T. ) ;
#44940=ORIENTED_EDGE ( 'NONE', *, *, #73942, .T. ) ;
#45104=LINE ( 'NONE', #287, #16155 ) ;
#45154=EDGE_CURVE ( 'NONE', #55933, #5623, #71743, .T. ) ;
#45165=AXIS2_PLACEMENT_3D ( 'NONE', #31680, #9338, #76833 ) ;
#45179=CARTESIAN_POINT ( 'NONE',  ( 0.5964549592197740946, 8.529703308962702124, 1.700000000000008837 ) ) ;
#45228=DIRECTION ( 'NONE',  ( -0.9890158633619158257, -0.1478094111296165414, -0.000000000000000000 ) ) ;
#45336=CARTESIAN_POINT ( 'NONE',  ( 0.1011420733776826480, 1.446399035885977069, -8.999999999999996447 ) ) ;
#45390=VERTEX_POINT ( 'NONE', #77046 ) ;
#45459=EDGE_LOOP ( 'NONE', ( #81175, #47829, #40694, #51694 ) ) ;
#45504=DIRECTION ( 'NONE',  ( 3.278764309610055092E-18, 4.688851412615178005E-17, -1.000000000000000000 ) ) ;
#45591=ORIENTED_EDGE ( 'NONE', *, *, #73549, .F. ) ;
#45720=EDGE_LOOP ( 'NONE', ( #92771, #50474, #24759, #95702 ) ) ;
#45785=CIRCLE ( 'NONE', #58987, 10.11363636363636154 ) ;
#45810=ORIENTED_EDGE ( 'NONE', *, *, #64042, .T. ) ;
#45812=CARTESIAN_POINT ( 'NONE',  ( -2.169994883066378222, 10.75358048763950869, -3.549999999999999822 ) ) ;
#46134=CARTESIAN_POINT ( 'NONE',  ( 1.876957540558651605, -5.558144974487054135, 0.000000000000000000 ) ) ;
#46139=DIRECTION ( 'NONE',  ( 1.000000000000000000, 0.000000000000000000, 4.335561085774420994E-16 ) ) ;
#46442=CYLINDRICAL_SURFACE ( 'NONE', #12629, 3.549999999999999378 ) ;
#46519=ADVANCED_FACE ( 'NONE', ( #86484 ), #78856, .T. ) ;
#46553=DIRECTION ( 'NONE',  ( 0.1478094111296165691, -0.9890158633619158257, 0.000000000000000000 ) ) ;
#46611=ORIENTED_EDGE ( 'NONE', *, *, #45154, .T. ) ;
#46709=EDGE_CURVE ( 'NONE', #74103, #94609, #5550, .T. ) ;
#46728=PLANE ( 'NONE',  #91956 ) ;
#46922=ORIENTED_EDGE ( 'NONE', *, *, #13322, .F. ) ;
#46925=ADVANCED_FACE ( 'NONE', ( #60551 ), #85866, .T. ) ;
#46952=DIRECTION ( 'NONE',  ( 0.1478094111296165691, -0.9890158633619158257, 0.000000000000000000 ) ) ;
#47374=DIRECTION ( 'NONE',  ( -0.06975647374412548285, -0.9975640502598241977, 0.000000000000000000 ) ) ;
#47438=ORIENTED_EDGE ( 'NONE', *, *, #53662, .F. ) ;
#47484=VERTEX_POINT ( 'NONE', #35845 ) ;
#47562=PLANE ( 'NONE',  #11394 ) ;
#47670=ADVANCED_FACE ( 'NONE', ( #41854 ), #26111, .F. ) ;
#47688=ORIENTED_EDGE ( 'NONE', *, *, #65712, .F. ) ;
#47757=DIRECTION ( 'NONE',  ( -0.000000000000000000, -0.000000000000000000, -1.000000000000000000 ) ) ;
#47829=ORIENTED_EDGE ( 'NONE', *, *, #49034, .T. ) ;
#47930=DIRECTION ( 'NONE',  ( -1.000000000000000000, 0.000000000000000000, 0.000000000000000000 ) ) ;
#48191=CIRCLE ( 'NONE', #64369, 2.899999999999999467 ) ;
#48193=CARTESIAN_POINT ( 'NONE',  ( 1.095236984349686971, 8.494825072090639750, 1.700000000000008837 ) ) ;
#48198=ORIENTED_EDGE ( 'NONE', *, *, #25508, .F. ) ;
#48234=DIRECTION ( 'NONE',  ( 0.000000000000000000, 0.000000000000000000, -1.000000000000000000 ) ) ;
#48313=DIRECTION ( 'NONE',  ( -0.8788171126619707119, 0.4771587602595986910, -0.000000000000000000 ) ) ;
#48345=ORIENTED_EDGE ( 'NONE', *, *, #42162, .T. ) ;
#48349=AXIS2_PLACEMENT_3D ( 'NONE', #37156, #83325, #21412 ) ;
#48379=CARTESIAN_POINT ( 'NONE',  ( -1.675486951385420475, 10.82748519320431591, -3.549999999999999822 ) ) ;
#48429=DIRECTION ( 'NONE',  ( -0.9975640502598243087, 0.06975647374412548285, 0.000000000000000000 ) ) ;
#48555=VECTOR ( 'NONE', #14860, 1000.000000000000000 ) ;
#48610=EDGE_LOOP ( 'NONE', ( #30117, #24228, #21305, #48198 ) ) ;
#48615=ORIENTED_EDGE ( 'NONE', *, *, #92283, .T. ) ;
#48645=AXIS2_PLACEMENT_3D ( 'NONE', #24009, #68201, #76779 ) ;
#48657=CARTESIAN_POINT ( 'NONE',  ( -1.164890887384984586, 4.028272616778473036, -3.549999999999999378 ) ) ;
#48671=ORIENTED_EDGE ( 'NONE', *, *, #46709, .T. ) ;
#48695=ORIENTED_EDGE ( 'NONE', *, *, #49672, .T. ) ;
#48811=DIRECTION ( 'NONE',  ( -0.2164396139380965478, 0.9762960071199346945, 0.000000000000000000 ) ) ;
#48858=DIRECTION ( 'NONE',  ( -1.000000000000000000, 0.000000000000000000, -4.956352788505167212E-16 ) ) ;
#48883=LINE ( 'NONE', #26029, #201 ) ;
#49034=EDGE_CURVE ( 'NONE', #1657, #24459, #51473, .T. ) ;
#49052=VECTOR ( 'NONE', #4587, 1000.000000000000114 ) ;
#49068=CARTESIAN_POINT ( 'NONE',  ( -4.531374827497722357, 4.263680106169587702, -1.700000000000009059 ) ) ;
#49184=VECTOR ( 'NONE', #25426, 1000.000000000000114 ) ;
#49187=DIRECTION ( 'NONE',  ( -1.000000000000000000, 0.000000000000000000, 0.000000000000000000 ) ) ;
#49312=ORIENTED_EDGE ( 'NONE', *, *, #60215, .T. ) ;
#49390=DIRECTION ( 'NONE',  ( 3.614007241618349141E-17, -9.637352644315597708E-17, -1.000000000000000000 ) ) ;
#49451=PLANE ( 'NONE',  #53467 ) ;
#49455=AXIS2_PLACEMENT_3D ( 'NONE', #2779, #73771, #26101 ) ;
#49466=DIRECTION ( 'NONE',  ( 3.278764309610055092E-18, 4.688851412615178005E-17, 1.000000000000000000 ) ) ;
#49530=DIRECTION ( 'NONE',  ( -0.06975647374412546897, -0.9975640502598241977, 4.700301109882543835E-17 ) ) ;
#49617=LINE ( 'NONE', #42006, #34379 ) ;
#49635=DIRECTION ( 'NONE',  ( -0.1478094111296165969, 0.9890158633619159367, 0.000000000000000000 ) ) ;
#49672=EDGE_CURVE ( 'NONE', #43797, #26418, #20700, .T. ) ;
#49713=DIRECTION ( 'NONE',  ( -1.084136044942898696E-16, -0.000000000000000000, 1.000000000000000000 ) ) ;
#49877=DIRECTION ( 'NONE',  ( 1.000000000000000000, 0.000000000000000000, 4.335561085774420994E-16 ) ) ;
#50036=ADVANCED_FACE ( 'NONE', ( #28568 ), #42815, .T. ) ;
#50146=VECTOR ( 'NONE', #50833, 1000.000000000000000 ) ;
#50199=AXIS2_PLACEMENT_3D ( 'NONE', #55408, #31550, #86345 ) ;
#50368=CARTESIAN_POINT ( 'NONE',  ( 4.143214286797170409, 4.821574250326515099, -3.549999999999999378 ) ) ;
#50435=ORIENTED_EDGE ( 'NONE', *, *, #9009, .F. ) ;
#50442=FACE_OUTER_BOUND ( 'NONE', #3208, .T. ) ;
#50474=ORIENTED_EDGE ( 'NONE', *, *, #67636, .T. ) ;
#50563=ORIENTED_EDGE ( 'NONE', *, *, #33872, .F. ) ;
#50621=CARTESIAN_POINT ( 'NONE',  ( -2.169994883066378222, 10.75358048763950869, 0.000000000000000000 ) ) ;
#50636=CARTESIAN_POINT ( 'NONE',  ( -3.302878749216429544, 14.80319218833827044, 8.673617379884035472E-16 ) ) ;
#50676=PRODUCT ( 'Tape Measure Hook', 'Tape Measure Hook', '', ( #79949 ) ) ;
#50816=ORIENTED_EDGE ( 'NONE', *, *, #93361, .F. ) ;
#50833=DIRECTION ( 'NONE',  ( 4.818676322157798854E-17, 0.000000000000000000, 1.000000000000000000 ) ) ;
#50870=ORIENTED_EDGE ( 'NONE', *, *, #25508, .T. ) ;
#50880=DIRECTION ( 'NONE',  ( 0.9762960071199348056, 0.2164396139380966033, -0.000000000000000000 ) ) ;
#50885=CARTESIAN_POINT ( 'NONE',  ( 1.437548984227666304, -5.319565594357255733, 0.000000000000000000 ) ) ;
#50938=CARTESIAN_POINT ( 'NONE',  ( 1.351731822651893733, -3.882286141751411179, 8.999999999999994671 ) ) ;
#51300=VERTEX_POINT ( 'NONE', #34347 ) ;
#51328=CARTESIAN_POINT ( 'NONE',  ( -0.3059464777392852941, -8.530684776139525027, -9.000000000000000000 ) ) ;
#51412=DIRECTION ( 'NONE',  ( -0.1478094111296165691, 0.9890158633619158257, 6.377659838150018832E-17 ) ) ;
#51423=CIRCLE ( 'NONE', #7666, 1.700000000000008837 ) ;
#51473=LINE ( 'NONE', #73802, #71916 ) ;
#51488=LINE ( 'NONE', #52990, #37388 ) ;
#51694=ORIENTED_EDGE ( 'NONE', *, *, #70217, .F. ) ;
#51735=ADVANCED_FACE ( 'NONE', ( #50442 ), #42841, .F. ) ;
#51793=AXIS2_PLACEMENT_3D ( 'NONE', #94966, #17850, #48811 ) ;
#51870=CARTESIAN_POINT ( 'NONE',  ( 10.57556460110582996, 0.7139560615726621151, -8.999999999999994671 ) ) ;
#51912=ORIENTED_EDGE ( 'NONE', *, *, #72683, .F. ) ;
#51929=CARTESIAN_POINT ( 'NONE',  ( 1.437548984227666304, -5.319565594357255733, 0.000000000000000000 ) ) ;
#51978=DIRECTION ( 'NONE',  ( 0.1478094111296165969, -0.9890158633619159367, 0.000000000000000000 ) ) ;
#52065=VERTEX_POINT ( 'NONE', #33971 ) ;
#52116=ADVANCED_FACE ( 'NONE', ( #90754 ), #27855, .T. ) ;
#52121=DIRECTION ( 'NONE',  ( -0.4771587602595987465, -0.8788171126619706008, 0.000000000000000000 ) ) ;
#52135=PLANE ( 'NONE',  #33407 ) ;
#52172=ORIENTED_EDGE ( 'NONE', *, *, #27112, .F. ) ;
#52432=LINE ( 'NONE', #45812, #17823 ) ;
#52569=ORIENTED_EDGE ( 'NONE', *, *, #38465, .T. ) ;
#52672=ORIENTED_EDGE ( 'NONE', *, *, #10138, .F. ) ;
#52723=DIRECTION ( 'NONE',  ( -0.1478094111296165691, 0.9890158633619158257, -0.000000000000000000 ) ) ;
#52789=VERTEX_POINT ( 'NONE', #62197 ) ;
#52964=CARTESIAN_POINT ( 'NONE',  ( 0.2450472757604428842, -5.405843919193451086, -9.000000000000000000 ) ) ;
#52990=CARTESIAN_POINT ( 'NONE',  ( 1.351731822651893733, -3.882286141751412067, -8.999999999999998224 ) ) ;
#53035=DIRECTION ( 'NONE',  ( 0.9890158633619159367, 0.1478094111296165969, 0.000000000000000000 ) ) ;
#53397=CIRCLE ( 'NONE', #9643, 2.899999999999999467 ) ;
#53467=AXIS2_PLACEMENT_3D ( 'NONE', #87496, #24085, #33713 ) ;
#53481=VECTOR ( 'NONE', #66181, 1000.000000000000114 ) ;
#53490=PLANE ( 'NONE',  #48645 ) ;
#53662=EDGE_CURVE ( 'NONE', #5623, #42138, #33357, .T. ) ;
#53717=CARTESIAN_POINT ( 'NONE',  ( 0.8635838190919263857, -3.990505948720459717, 8.999999999999994671 ) ) ;
#53880=EDGE_LOOP ( 'NONE', ( #81331, #49312, #8345, #5768 ) ) ;
#53921=DIRECTION ( 'NONE',  ( -0.06975647374412546897, -0.9975640502598241977, 4.700301109882544451E-17 ) ) ;
#53940=AXIS2_PLACEMENT_3D ( 'NONE', #51929, #37688, #92462 ) ;
#53991=ORIENTED_EDGE ( 'NONE', *, *, #3104, .F. ) ;
#54188=ORIENTED_EDGE ( 'NONE', *, *, #39354, .T. ) ;
#54345=FACE_OUTER_BOUND ( 'NONE', #84004, .T. ) ;
#54431=AXIS2_PLACEMENT_3D ( 'NONE', #70203, #8300, #86425 ) ;
#54493=ADVANCED_FACE ( 'NONE', ( #54984 ), #56500, .T. ) ;
#54502=VECTOR ( 'NONE', #99853, 1000.000000000000000 ) ;
#54584=PLANE ( 'NONE',  #24274 ) ;
#54654=VECTOR ( 'NONE', #45228, 1000.000000000000114 ) ;
#54759=FACE_OUTER_BOUND ( 'NONE', #23589, .T. ) ;
#54883=EDGE_CURVE ( 'NONE', #19708, #13572, #13935, .T. ) ;
#54932=CARTESIAN_POINT ( 'NONE',  ( -2.717543299849222826, 17.80004702990586196, 0.000000000000000000 ) ) ;
#54938=DIRECTION ( 'NONE',  ( -0.4771587602595988020, -0.8788171126619706008, -0.000000000000000000 ) ) ;
#54984=FACE_OUTER_BOUND ( 'NONE', #18988, .T. ) ;
#55002=EDGE_CURVE ( 'NONE', #16487, #55933, #8186, .T. ) ;
#55165=ADVANCED_FACE ( 'NONE', ( #60868 ), #99890, .T. ) ;
#55217=CYLINDRICAL_SURFACE ( 'NONE', #57853, 10.11363636363636331 ) ;
#55262=DIRECTION ( 'NONE',  ( 1.000000000000000000, 0.000000000000000000, -0.000000000000000000 ) ) ;
#55408=CARTESIAN_POINT ( 'NONE',  ( -4.700032041049139409, -6.144890974841530351, -9.000000000000000000 ) ) ;
#55537=CYLINDRICAL_SURFACE ( 'NONE', #45165, 5.000000000000001776 ) ;
#55552=CARTESIAN_POINT ( 'NONE',  ( -2.814730745656462307, 14.91141199530731853, 8.673617379884035472E-16 ) ) ;
#55580=ORIENTED_EDGE ( 'NONE', *, *, #57989, .F. ) ;
#55595=DIRECTION ( 'NONE',  ( -0.9890158633619159367, -0.1478094111296165969, 0.000000000000000000 ) ) ;
#55598=VERTEX_POINT ( 'NONE', #82075 ) ;
#55788=DIRECTION ( 'NONE',  ( 0.06975647374412523305, 0.9975640502598241977, 0.000000000000000000 ) ) ;
#55882=ADVANCED_FACE ( 'NONE', ( #64263 ), #2347, .F. ) ;
#55894=EDGE_CURVE ( 'NONE', #85639, #1549, #26679, .T. ) ;
#55907=ORIENTED_EDGE ( 'NONE', *, *, #30882, .F. ) ;
#55933=VERTEX_POINT ( 'NONE', #95686 ) ;
#55980=ORIENTED_EDGE ( 'NONE', *, *, #95147, .T. ) ;
#56021=CARTESIAN_POINT ( 'NONE',  ( 1.095236984349686749, 8.494825072090636198, 1.700000000000008393 ) ) ;
#56032=ORIENTED_EDGE ( 'NONE', *, *, #16995, .F. ) ;
#56110=CIRCLE ( 'NONE', #26907, 10.49999999999999112 ) ;
#56126=ORIENTED_EDGE ( 'NONE', *, *, #23680, .F. ) ;
#56437=CARTESIAN_POINT ( 'NONE',  ( 1.876957540558651605, -5.558144974487054135, 0.000000000000000000 ) ) ;
#56481=ADVANCED_FACE ( 'NONE', ( #79592 ), #10084, .F. ) ;
#56500=PLANE ( 'NONE',  #54431 ) ;
#56646=CARTESIAN_POINT ( 'NONE',  ( -4.700032041049139409, -6.144890974841530351, 8.999999999999998224 ) ) ;
#57026=PRODUCT_DEFINITION_FORMATION_WITH_SPECIFIED_SOURCE ( 'ANY', '', #50676, .NOT_KNOWN. ) ;
#57052=FACE_OUTER_BOUND ( 'NONE', #19453, .T. ) ;
#57144=CARTESIAN_POINT ( 'NONE',  ( 0.5964549592197745387, 8.529703308962702124, -1.700000000000008837 ) ) ;
#57357=CARTESIAN_POINT ( 'NONE',  ( 1.259127588940877285, 10.83856991095998801, 0.000000000000000000 ) ) ;
#57377=DIRECTION ( 'NONE',  ( -0.9975640502598241977, 0.06975647374412534407, -4.324999876874012340E-16 ) ) ;
#57418=DIRECTION ( 'NONE',  ( -0.2164396139380966033, 0.9762960071199348056, -0.000000000000000000 ) ) ;
#57470=ORIENTED_EDGE ( 'NONE', *, *, #30882, .T. ) ;
#57509=EDGE_LOOP ( 'NONE', ( #52172, #39964, #48671, #86118 ) ) ;
#57853=AXIS2_PLACEMENT_3D ( 'NONE', #2422, #18136, #26252 ) ;
#57989=EDGE_CURVE ( 'NONE', #64635, #77501, #28022, .T. ) ;
#58044=DIRECTION ( 'NONE',  ( 4.335561085774420994E-16, 0.000000000000000000, -1.000000000000000000 ) ) ;
#58061=CARTESIAN_POINT ( 'NONE',  ( -4.209565145052936330, 8.865772972990910716, 1.700000000000008837 ) ) ;
#58108=DIRECTION ( 'NONE',  ( 0.9890158633619159367, 0.1478094111296165969, 0.000000000000000000 ) ) ;
#58202=VERTEX_POINT ( 'NONE', #16782 ) ;
#58380=EDGE_CURVE ( 'NONE', #29853, #82528, #75636, .T. ) ;
#58387=CARTESIAN_POINT ( 'NONE',  ( 0.4987820251299121543, -0.03487823687206273449, -9.000000000000000000 ) ) ;
#58549=LINE ( 'NONE', #58061, #53481 ) ;
#58622=DIRECTION ( 'NONE',  ( 0.9890158633619158257, 0.1478094111296165136, 0.000000000000000000 ) ) ;
#58840=CARTESIAN_POINT ( 'NONE',  ( -1.382686142301752019, 8.868309232919825646, -9.000000000000000000 ) ) ;
#58987=AXIS2_PLACEMENT_3D ( 'NONE', #35408, #83045, #52121 ) ;
#59025=FACE_OUTER_BOUND ( 'NONE', #82087, .T. ) ;
#59028=DIRECTION ( 'NONE',  ( 0.06975647374412549673, 0.9975640502598241977, 0.000000000000000000 ) ) ;
#59074=ORIENTED_EDGE ( 'NONE', *, *, #12078, .F. ) ;
#59132=DIRECTION ( 'NONE',  ( -9.527529159155689202E-17, 4.297590679709308564E-16, 1.000000000000000000 ) ) ;
#59153=ORIENTED_EDGE ( 'NONE', *, *, #16568, .F. ) ;
#59310=VERTEX_POINT ( 'NONE', #98029 ) ;
#59535=AXIS2_PLACEMENT_3D ( 'NONE', #6432, #12160, #89299 ) ;
#59605=CARTESIAN_POINT ( 'NONE',  ( 10.57556460110582996, 0.7139560615726621151, -8.999999999999991118 ) ) ;
#59652=CARTESIAN_POINT ( 'NONE',  ( 0.5999240985075944277, 1.411520799013914917, -8.999999999999998224 ) ) ;
#59817=EDGE_CURVE ( 'NONE', #43562, #70264, #71309, .T. ) ;
#60135=PLANE ( 'NONE',  #25761 ) ;
#60215=EDGE_CURVE ( 'NONE', #52789, #28486, #23968, .T. ) ;
#60404=DIRECTION ( 'NONE',  ( 0.9890158633619159367, 0.1478094111296165969, 0.000000000000000000 ) ) ;
#60432=VECTOR ( 'NONE', #82201, 1000.000000000000114 ) ;
#60551=FACE_OUTER_BOUND ( 'NONE', #57509, .T. ) ;
#60612=VECTOR ( 'NONE', #27331, 999.9999999999998863 ) ;
#60868=FACE_OUTER_BOUND ( 'NONE', #63036, .T. ) ;
#60871=CARTESIAN_POINT ( 'NONE',  ( 0.5999240985075874333, 1.411520799013914917, 8.999999999999987566 ) ) ;
#60881=AXIS2_PLACEMENT_3D ( 'NONE', #86481, #16967, #47930 ) ;
#61010=AXIS2_PLACEMENT_3D ( 'NONE', #25150, #95175, #1333 ) ;
#61030=LINE ( 'NONE', #17731, #34064 ) ;
#61233=FACE_OUTER_BOUND ( 'NONE', #97414, .T. ) ;
#61635=CARTESIAN_POINT ( 'NONE',  ( 1.754398552524170762, 17.92127466780477718, 9.000000000000000000 ) ) ;
#61709=EDGE_CURVE ( 'NONE', #74792, #55598, #39096, .T. ) ;
#61725=EDGE_CURVE ( 'NONE', #24459, #41863, #10903, .T. ) ;
#61769=LINE ( 'NONE', #77459, #39640 ) ;
#61784=VECTOR ( 'NONE', #50880, 1000.000000000000000 ) ;
#61988=AXIS2_PLACEMENT_3D ( 'NONE', #96191, #11943, #88579 ) ;
#62013=DIRECTION ( 'NONE',  ( -0.8788171126619707119, 0.4771587602595986910, -0.000000000000000000 ) ) ;
#62120=CARTESIAN_POINT ( 'NONE',  ( 0.1334620785917008390, -8.769264156269324317, 8.999999999999998224 ) ) ;
#62149=ADVANCED_FACE ( 'NONE', ( #64358 ), #17652, .F. ) ;
#62197=CARTESIAN_POINT ( 'NONE',  ( -0.3059464777392844059, -8.530684776139525027, 8.999999999999998224 ) ) ;
#62235=CARTESIAN_POINT ( 'NONE',  ( 0.8126045299064830196, -1.450440077808301975, 8.999999999999987566 ) ) ;
#62387=DIRECTION ( 'NONE',  ( 0.9975640502598243087, -0.06975647374412546897, -0.000000000000000000 ) ) ;
#62577=CARTESIAN_POINT ( 'NONE',  ( 1.095236984349686971, 8.494825072090639750, -1.700000000000008837 ) ) ;
#62648=ADVANCED_FACE ( 'NONE', ( #18896 ), #80304, .T. ) ;
#62670=ORIENTED_EDGE ( 'NONE', *, *, #15691, .T. ) ;
#62924=DIRECTION ( 'NONE',  ( -4.335561085774420994E-16, -0.000000000000000000, 1.000000000000000000 ) ) ;
#62933=EDGE_LOOP ( 'NONE', ( #83345, #3442, #92126, #11106 ) ) ;
#62995=EDGE_CURVE ( 'NONE', #13572, #89454, #17791, .T. ) ;
#63009=CARTESIAN_POINT ( 'NONE',  ( 1.351731822651893733, -3.882286141751412067, -8.999999999999998224 ) ) ;
#63036=EDGE_LOOP ( 'NONE', ( #48615, #87467, #21589, #75750 ) ) ;
#63048=LINE ( 'NONE', #40195, #39726 ) ;
#63052=VECTOR ( 'NONE', #51412, 1000.000000000000114 ) ;
#63120=DIRECTION ( 'NONE',  ( -0.9890158633619158257, -0.1478094111296165414, -0.000000000000000000 ) ) ;
#63225=ORIENTED_EDGE ( 'NONE', *, *, #77025, .F. ) ;
#63274=( NAMED_UNIT ( * ) PLANE_ANGLE_UNIT ( ) SI_UNIT ( $, .RADIAN. ) );
#63394=VECTOR ( 'NONE', #65124, 1000.000000000000114 ) ;
#63447=DIRECTION ( 'NONE',  ( 0.000000000000000000, 0.000000000000000000, 1.000000000000000000 ) ) ;
#63461=VECTOR ( 'NONE', #75441, 1000.000000000000000 ) ;
#63510=ORIENTED_EDGE ( 'NONE', *, *, #58380, .F. ) ;
#63546=ADVANCED_FACE ( 'NONE', ( #93599 ), #46442, .F. ) ;
#63558=ORIENTED_EDGE ( 'NONE', *, *, #44533, .T. ) ;
#63728=EDGE_LOOP ( 'NONE', ( #29617, #99179, #45810, #86426 ) ) ;
#63786=AXIS2_PLACEMENT_3D ( 'NONE', #69580, #63, #96913 ) ;
#63804=DIRECTION ( 'NONE',  ( -0.9890158633619159367, -0.1478094111296165969, 0.000000000000000000 ) ) ;
#63949=VECTOR ( 'NONE', #76687, 1000.000000000000227 ) ;
#64042=EDGE_CURVE ( 'NONE', #43797, #69058, #74265, .T. ) ;
#64255=DIRECTION ( 'NONE',  ( -0.000000000000000000, -0.000000000000000000, -1.000000000000000000 ) ) ;
#64263=FACE_OUTER_BOUND ( 'NONE', #45720, .T. ) ;
#64349=LINE ( 'NONE', #1930, #84683 ) ;
#64358=FACE_OUTER_BOUND ( 'NONE', #53880, .T. ) ;
#64369=AXIS2_PLACEMENT_3D ( 'NONE', #13525, #89672, #67341 ) ;
#64397=CARTESIAN_POINT ( 'NONE',  ( -4.700032041049139409, -6.144890974841530351, 9.000000000000000000 ) ) ;
#64469=DIRECTION ( 'NONE',  ( -0.06975647374412549673, -0.9975640502598241977, 0.000000000000000000 ) ) ;
#64543=CARTESIAN_POINT ( 'NONE',  ( 0.4987820251299121543, -0.03487823687206274836, 9.000000000000000000 ) ) ;
#64608=EDGE_CURVE ( 'NONE', #75345, #51300, #7839, .T. ) ;
#64635=VERTEX_POINT ( 'NONE', #32933 ) ;
#64702=ADVANCED_FACE ( 'NONE', ( #15701 ), #94320, .F. ) ;
#64761=ADVANCED_FACE ( 'NONE', ( #69989 ), #31934, .F. ) ;
#64777=LINE ( 'NONE', #10958, #24845 ) ;
#64902=CARTESIAN_POINT ( 'NONE',  ( -4.045674540461745572, 11.20951781186025897, 0.000000000000000000 ) ) ;
#64909=CARTESIAN_POINT ( 'NONE',  ( 0.8635838190919263857, -3.990505948720460605, -8.999999999999998224 ) ) ;
#64967=DIRECTION ( 'NONE',  ( 0.9975640502598243087, -0.06975647374412546897, -0.000000000000000000 ) ) ;
#65084=VECTOR ( 'NONE', #47757, 1000.000000000000000 ) ;
#65124=DIRECTION ( 'NONE',  ( -0.1478094111296165691, 0.9890158633619158257, -6.377659838150018832E-17 ) ) ;
#65338=ORIENTED_EDGE ( 'NONE', *, *, #25021, .F. ) ;
#65452=DIRECTION ( 'NONE',  ( -1.084136044942898696E-16, -0.000000000000000000, 1.000000000000000000 ) ) ;
#65503=ADVANCED_FACE ( 'NONE', ( #78342 ), #55537, .F. ) ;
#65671=FACE_BOUND ( 'NONE', #77494, .T. ) ;
#65712=EDGE_CURVE ( 'NONE', #59310, #82863, #81858, .T. ) ;
#65795=ORIENTED_EDGE ( 'NONE', *, *, #15691, .F. ) ;
#65818=ORIENTED_EDGE ( 'NONE', *, *, #40054, .F. ) ;
#66038=LINE ( 'NONE', #64543, #42096 ) ;
#66167=ORIENTED_EDGE ( 'NONE', *, *, #40054, .T. ) ;
#66181=DIRECTION ( 'NONE',  ( 0.9975640502598241977, -0.06975647374412546897, -0.000000000000000000 ) ) ;
#66214=DIRECTION ( 'NONE',  ( -0.9890158633619158257, -0.1478094111296165414, -0.000000000000000000 ) ) ;
#66353=DIRECTION ( 'NONE',  ( 0.1478094111296165691, -0.9890158633619158257, -6.377659838150018832E-17 ) ) ;
#66468=EDGE_CURVE ( 'NONE', #85639, #97920, #11484, .T. ) ;
#66650=( NAMED_UNIT ( * ) SI_UNIT ( $, .STERADIAN. ) SOLID_ANGLE_UNIT ( ) );
#66669=VECTOR ( 'NONE', #63120, 1000.000000000000114 ) ;
#66778=EDGE_LOOP ( 'NONE', ( #15594, #6721, #91144, #39228 ) ) ;
#66856=VECTOR ( 'NONE', #89075, 1000.000000000000114 ) ;
#66969=VECTOR ( 'NONE', #52723, 1000.000000000000114 ) ;
#67027=ADVANCED_BREP_SHAPE_REPRESENTATION ( '', ( #10173, #37391 ), #14765 ) ;
#67029=VECTOR ( 'NONE', #14528, 1000.000000000000114 ) ;
#67072=ORIENTED_EDGE ( 'NONE', *, *, #93361, .T. ) ;
#67112=CARTESIAN_POINT ( 'NONE',  ( 0.8635838190919263857, -3.990505948720460605, -8.999999999999998224 ) ) ;
#67137=EDGE_CURVE ( 'NONE', #18856, #94609, #63048, .T. ) ;
#67341=DIRECTION ( 'NONE',  ( -0.06975647374412549673, -0.9975640502598241977, 0.000000000000000000 ) ) ;
#67374=LINE ( 'NONE', #98292, #49184 ) ;
#67636=EDGE_CURVE ( 'NONE', #55933, #12105, #98095, .T. ) ;
#67869=VERTEX_POINT ( 'NONE', #8095 ) ;
#68100=VECTOR ( 'NONE', #75417, 1000.000000000000000 ) ;
#68103=PLANE ( 'NONE',  #14827 ) ;
#68138=DIRECTION ( 'NONE',  ( -0.9890158633619160478, -0.1478094111296159863, 0.000000000000000000 ) ) ;
#68201=DIRECTION ( 'NONE',  ( -0.9975640502598243087, 0.06975647374412548285, 0.000000000000000000 ) ) ;
#68635=FACE_OUTER_BOUND ( 'NONE', #83703, .T. ) ;
#69058=VERTEX_POINT ( 'NONE', #12831 ) ;
#69114=VECTOR ( 'NONE', #54938, 999.9999999999998863 ) ;
#69144=LINE ( 'NONE', #54932, #9851 ) ;
#69151=CARTESIAN_POINT ( 'NONE',  ( -0.7638880233336636794, -9.374108182320437521, 9.000000000000000000 ) ) ;
#69285=ORIENTED_EDGE ( 'NONE', *, *, #49034, .F. ) ;
#69301=DIRECTION ( 'NONE',  ( 1.084136044942898696E-16, 0.000000000000000000, -1.000000000000000000 ) ) ;
#69343=VECTOR ( 'NONE', #57377, 1000.000000000000114 ) ;
#69352=FACE_OUTER_BOUND ( 'NONE', #63728, .T. ) ;
#69400=ORIENTED_EDGE ( 'NONE', *, *, #95147, .F. ) ;
#69515=ORIENTED_EDGE ( 'NONE', *, *, #66468, .T. ) ;
#69519=ORIENTED_EDGE ( 'NONE', *, *, #83955, .F. ) ;
#69532=ORIENTED_EDGE ( 'NONE', *, *, #42162, .F. ) ;
#69580=CARTESIAN_POINT ( 'NONE',  ( -3.302878749216429544, 14.80319218833827044, 8.673617379884035472E-16 ) ) ;
#69584=DIRECTION ( 'NONE',  ( 0.9890158633619158257, 0.1478094111296165136, 0.000000000000000000 ) ) ;
#69676=ORIENTED_EDGE ( 'NONE', *, *, #13464, .F. ) ;
#69840=FACE_OUTER_BOUND ( 'NONE', #48610, .T. ) ;
#69975=CIRCLE ( 'NONE', #26232, 3.549999999999999378 ) ;
#69989=FACE_OUTER_BOUND ( 'NONE', #81241, .T. ) ;
#70203=CARTESIAN_POINT ( 'NONE',  ( 1.754398552524170762, 17.92127466780477718, -9.000000000000000000 ) ) ;
#70217=EDGE_CURVE ( 'NONE', #14465, #41863, #58549, .T. ) ;
#70264=VERTEX_POINT ( 'NONE', #50938 ) ;
#70284=DIRECTION ( 'NONE',  ( -0.9890158633619159367, -0.1478094111296165691, -0.000000000000000000 ) ) ;
#70474=DIRECTION ( 'NONE',  ( 0.000000000000000000, 0.000000000000000000, 1.000000000000000000 ) ) ;
#70549=ORIENTED_EDGE ( 'NONE', *, *, #72147, .T. ) ;
#70706=AXIS2_PLACEMENT_3D ( 'NONE', #64397, #25294, #25800 ) ;
#70733=AXIS2_PLACEMENT_3D ( 'NONE', #2481, #77576, #1984 ) ;
#70960=LINE ( 'NONE', #79054, #16070 ) ;
#71015=CARTESIAN_POINT ( 'NONE',  ( -4.209565145052936330, 8.865772972990910716, -1.700000000000008837 ) ) ;
#71127=CARTESIAN_POINT ( 'NONE',  ( -2.948852648430471124, -14.44618168209107445, 0.000000000000000000 ) ) ;
#71137=ORIENTED_EDGE ( 'NONE', *, *, #88395, .T. ) ;
#71138=LINE ( 'NONE', #79235, #95538 ) ;
#71309=LINE ( 'NONE', #53717, #54502 ) ;
#71313=CARTESIAN_POINT ( 'NONE',  ( -1.382686142301752019, 8.868309232919825646, 0.000000000000000000 ) ) ;
#71317=EDGE_CURVE ( 'NONE', #16487, #76018, #90767, .T. ) ;
#71547=CYLINDRICAL_SURFACE ( 'NONE', #42270, 3.549999999999999378 ) ;
#71743=LINE ( 'NONE', #2237, #86388 ) ;
#71772=DIRECTION ( 'NONE',  ( -0.2164396139380966033, 0.9762960071199348056, 0.000000000000000000 ) ) ;
#71794=CARTESIAN_POINT ( 'NONE',  ( -4.209565145052936330, 8.865772972990910716, 1.700000000000008837 ) ) ;
#71900=FACE_BOUND ( 'NONE', #33886, .T. ) ;
#71916=VECTOR ( 'NONE', #75289, 1000.000000000000114 ) ;
#71942=ORIENTED_EDGE ( 'NONE', *, *, #53662, .T. ) ;
#72052=DIRECTION ( 'NONE',  ( -0.9890158633619159367, -0.1478094111296165691, -0.000000000000000000 ) ) ;
#72147=EDGE_CURVE ( 'NONE', #51300, #45390, #81560, .T. ) ;
#72296=ORIENTED_EDGE ( 'NONE', *, *, #30994, .T. ) ;
#72302=EDGE_CURVE ( 'NONE', #52789, #43797, #98255, .T. ) ;
#72407=ORIENTED_EDGE ( 'NONE', *, *, #73549, .T. ) ;
#72491=CYLINDRICAL_SURFACE ( 'NONE', #20784, 2.899999999999999467 ) ;
#72683=EDGE_CURVE ( 'NONE', #19708, #78060, #51488, .T. ) ;
#72715=ADVANCED_FACE ( 'NONE', ( #27654 ), #43873, .F. ) ;
#72723=ORIENTED_EDGE ( 'NONE', *, *, #89409, .T. ) ;
#72761=EDGE_CURVE ( 'NONE', #82528, #76018, #186, .T. ) ;
#72812=CARTESIAN_POINT ( 'NONE',  ( 4.143214286797170409, 4.821574250326516875, 3.549999999999996714 ) ) ;
#72854=CARTESIAN_POINT ( 'NONE',  ( 0.8635838190919263857, -3.990505948720459717, 8.999999999999994671 ) ) ;
#72993=FACE_OUTER_BOUND ( 'NONE', #1, .T. ) ;
#73049=CARTESIAN_POINT ( 'NONE',  ( -0.7395115731254272573, 18.09566585216508727, 8.999999999999998224 ) ) ;
#73365=UNCERTAINTY_MEASURE_WITH_UNIT (LENGTH_MEASURE( 1.000000000000000082E-05 ), #89951, 'distance_accuracy_value', 'NONE');
#73374=EDGE_CURVE ( 'NONE', #55933, #92378, #40140, .T. ) ;
#73400=ORIENTED_EDGE ( 'NONE', *, *, #92201, .T. ) ;
#73549=EDGE_CURVE ( 'NONE', #69058, #81283, #12674, .T. ) ;
#73691=DIRECTION ( 'NONE',  ( -4.335561085774420994E-16, -0.000000000000000000, 1.000000000000000000 ) ) ;
#73771=DIRECTION ( 'NONE',  ( -1.084136044942898696E-16, -0.000000000000000000, 1.000000000000000000 ) ) ;
#73802=CARTESIAN_POINT ( 'NONE',  ( -3.843380766603781584, 14.10245355761374775, 0.000000000000000000 ) ) ;
#73935=ORIENTED_EDGE ( 'NONE', *, *, #61725, .F. ) ;
#73942=EDGE_CURVE ( 'NONE', #25637, #52065, #97433, .T. ) ;
#74103=VERTEX_POINT ( 'NONE', #5816 ) ;
#74118=CARTESIAN_POINT ( 'NONE',  ( 0.7734273019049007214, 3.892732205269316292, -1.700000000000009059 ) ) ;
#74234=EDGE_CURVE ( 'NONE', #75345, #17858, #30653, .T. ) ;
#74265=CIRCLE ( 'NONE', #48349, 5.500000000000001776 ) ;
#74310=EDGE_LOOP ( 'NONE', ( #18314, #8876, #72296, #28959 ) ) ;
#74344=AXIS2_PLACEMENT_3D ( 'NONE', #99913, #60404, #14191 ) ;
#74568=ADVANCED_FACE ( 'NONE', ( #37140 ), #68103, .T. ) ;
#74576=DIRECTION ( 'NONE',  ( -0.000000000000000000, -0.000000000000000000, -1.000000000000000000 ) ) ;
#74594=ORIENTED_EDGE ( 'NONE', *, *, #71317, .T. ) ;
#74731=DIRECTION ( 'NONE',  ( -0.9762960071199348056, -0.2164396139380965756, -4.956352788505166226E-16 ) ) ;
#74792=VERTEX_POINT ( 'NONE', #97918 ) ;
#74796=VECTOR ( 'NONE', #4837, 1000.000000000000000 ) ;
#74947=EDGE_CURVE ( 'NONE', #55598, #59310, #69975, .T. ) ;
#75241=AXIS2_PLACEMENT_3D ( 'NONE', #24785, #70474, #55262 ) ;
#75289=DIRECTION ( 'NONE',  ( 0.9975640502598241977, -0.06975647374412546897, -0.000000000000000000 ) ) ;
#75345=VERTEX_POINT ( 'NONE', #92188 ) ;
#75417=DIRECTION ( 'NONE',  ( 0.8788171126619707119, -0.4771587602595986910, 6.123031769111886291E-17 ) ) ;
#75423=LINE ( 'NONE', #82548, #67029 ) ;
#75441=DIRECTION ( 'NONE',  ( 0.2164396139380966033, -0.9762960071199348056, 4.401934094135205585E-16 ) ) ;
#75636=CIRCLE ( 'NONE', #12261, 9.999999999999991118 ) ;
#75642=EDGE_CURVE ( 'NONE', #77501, #55598, #11660, .T. ) ;
#75750=ORIENTED_EDGE ( 'NONE', *, *, #31022, .T. ) ;
#75826=FACE_OUTER_BOUND ( 'NONE', #87009, .T. ) ;
#76018=VERTEX_POINT ( 'NONE', #41135 ) ;
#76025=FACE_OUTER_BOUND ( 'NONE', #93909, .T. ) ;
#76144=ORIENTED_EDGE ( 'NONE', *, *, #88693, .F. ) ;
#76192=CIRCLE ( 'NONE', #3374, 3.549999999999999378 ) ;
#76232=ADVANCED_FACE ( 'NONE', ( #61233 ), #6431, .F. ) ;
#76394=CARTESIAN_POINT ( 'NONE',  ( -4.700032041049139409, -6.144890974841530351, 8.999999999999998224 ) ) ;
#76615=EDGE_LOOP ( 'NONE', ( #51912, #87777, #50563, #24581 ) ) ;
#76687=DIRECTION ( 'NONE',  ( 0.9975640502598247528, -0.06975647374411753088, 0.000000000000000000 ) ) ;
#76779=DIRECTION ( 'NONE',  ( -0.06975647374412546897, -0.9975640502598241977, 0.000000000000000000 ) ) ;
#76833=DIRECTION ( 'NONE',  ( 0.8788171126619707119, -0.4771587602595985800, 0.000000000000000000 ) ) ;
#76867=DIRECTION ( 'NONE',  ( 0.1478094111296165969, -0.9890158633619159367, 0.000000000000000000 ) ) ;
#76889=DIRECTION ( 'NONE',  ( -1.000000000000000000, 0.000000000000000000, 0.000000000000000000 ) ) ;
#77025=EDGE_CURVE ( 'NONE', #12105, #42138, #11677, .T. ) ;
#77046=CARTESIAN_POINT ( 'NONE',  ( -0.6703829557040269504, 4.102177322343282917, 3.549999999999996714 ) ) ;
#77146=VECTOR ( 'NONE', #43442, 1000.000000000000114 ) ;
#77255=CIRCLE ( 'NONE', #33537, 3.549999999999999378 ) ;
#77459=CARTESIAN_POINT ( 'NONE',  ( 1.095236984349686971, 8.494825072090639750, -1.700000000000008837 ) ) ;
#77489=EDGE_LOOP ( 'NONE', ( #46922, #5767, #37602, #86272 ) ) ;
#77494=EDGE_LOOP ( 'NONE', ( #85483, #17799, #93109, #4631, #4553 ) ) ;
#77501=VERTEX_POINT ( 'NONE', #48657 ) ;
#77551=CARTESIAN_POINT ( 'NONE',  ( 10.57556460110582286, 0.7139560615726621151, 8.999999999999994671 ) ) ;
#77576=DIRECTION ( 'NONE',  ( 9.426781450619601849E-18, -6.307606751056558338E-17, -1.000000000000000000 ) ) ;
#77793=DIRECTION ( 'NONE',  ( 0.9975640502598243087, -0.06975647374412546897, -0.000000000000000000 ) ) ;
#77965=DIRECTION ( 'NONE',  ( -0.9762960071199348056, -0.2164396139380966033, 6.123031769111886291E-17 ) ) ;
#77993=VECTOR ( 'NONE', #74576, 1000.000000000000000 ) ;
#78008=DIRECTION ( 'NONE',  ( -4.335561085774420994E-16, -0.000000000000000000, 1.000000000000000000 ) ) ;
#78060=VERTEX_POINT ( 'NONE', #63009 ) ;
#78242=DIRECTION ( 'NONE',  ( -0.000000000000000000, 0.000000000000000000, 1.000000000000000000 ) ) ;
#78342=FACE_OUTER_BOUND ( 'NONE', #92100, .T. ) ;
#78432=CYLINDRICAL_SURFACE ( 'NONE', #61010, 3.549999999999999378 ) ;
#78797=AXIS2_PLACEMENT_3D ( 'NONE', #56646, #42428, #17057 ) ;
#78856=PLANE ( 'NONE',  #3915 ) ;
#79002=AXIS2_PLACEMENT_3D ( 'NONE', #18635, #34377, #17645 ) ;
#79054=CARTESIAN_POINT ( 'NONE',  ( 0.1334620785917004226, -8.769264156269324317, 8.401340300369719094E-17 ) ) ;
#79235=CARTESIAN_POINT ( 'NONE',  ( 0.9317375178030620209, -7.299023693294228288, -9.000000000000000000 ) ) ;
#79369=ORIENTED_EDGE ( 'NONE', *, *, #37308, .T. ) ;
#79592=FACE_OUTER_BOUND ( 'NONE', #16260, .T. ) ;
#79599=CARTESIAN_POINT ( 'NONE',  ( -4.531374827497722357, 4.263680106169587702, -2.677392948487098267E-15 ) ) ;
#79609=CARTESIAN_POINT ( 'NONE',  ( 0.8126045299064900140, -1.450440077808301975, -8.999999999999998224 ) ) ;
#79639=CARTESIAN_POINT ( 'NONE',  ( 3.138110291115776995, 11.54688212118755075, 0.000000000000000000 ) ) ;
#79949=MECHANICAL_CONTEXT ( 'NONE', #7717, 'mechanical' ) ;
#79997=DIRECTION ( 'NONE',  ( 0.9975640502598241977, -0.06975647374412546897, -0.000000000000000000 ) ) ;
#80050=DIRECTION ( 'NONE',  ( -1.000000000000000000, 0.000000000000000000, -0.000000000000000000 ) ) ;
#80304=PLANE ( 'NONE',  #28785 ) ;
#80323=VECTOR ( 'NONE', #27697, 1000.000000000000114 ) ;
#80347=CARTESIAN_POINT ( 'NONE',  ( 1.754398552524170762, 17.92127466780477718, 9.000000000000000000 ) ) ;
#80794=AXIS2_PLACEMENT_3D ( 'NONE', #92818, #17201, #93318 ) ;
#80826=LINE ( 'NONE', #48379, #63394 ) ;
#80855=DIRECTION ( 'NONE',  ( -1.000000000000000000, 0.000000000000000000, -0.000000000000000000 ) ) ;
#80866=ADVANCED_FACE ( 'NONE', ( #14395, #14893 ), #53490, .F. ) ;
#80964=CARTESIAN_POINT ( 'NONE',  ( -2.717543299849222826, 17.80004702990586196, 9.000000000000000000 ) ) ;
#81065=AXIS2_PLACEMENT_3D ( 'NONE', #92740, #78008, #907 ) ;
#81109=CARTESIAN_POINT ( 'NONE',  ( -0.7395115731254272573, 18.09566585216508727, 8.999999999999998224 ) ) ;
#81175=ORIENTED_EDGE ( 'NONE', *, *, #88894, .F. ) ;
#81241=EDGE_LOOP ( 'NONE', ( #70549, #50870, #82536, #65338 ) ) ;
#81283=VERTEX_POINT ( 'NONE', #30502 ) ;
#81331=ORIENTED_EDGE ( 'NONE', *, *, #72302, .F. ) ;
#81429=ORIENTED_EDGE ( 'NONE', *, *, #55002, .T. ) ;
#81560=LINE ( 'NONE', #12035, #17902 ) ;
#81590=CARTESIAN_POINT ( 'NONE',  ( -1.877194073982709988, 8.794404527355018431, -9.000000000000000000 ) ) ;
#81686=AXIS2_PLACEMENT_3D ( 'NONE', #56437, #48313, #8242 ) ;
#81858=LINE ( 'NONE', #4739, #63052 ) ;
#81922=CIRCLE ( 'NONE', #31725, 3.549999999999999378 ) ;
#82014=EDGE_CURVE ( 'NONE', #82863, #17858, #76192, .T. ) ;
#82075=CARTESIAN_POINT ( 'NONE',  ( -0.6401674778748456252, 0.5172663018436739479, -2.677392948487098267E-15 ) ) ;
#82082=DIRECTION ( 'NONE',  ( 0.000000000000000000, 0.000000000000000000, 1.000000000000000000 ) ) ;
#82087=EDGE_LOOP ( 'NONE', ( #42979, #91737, #87724, #8961 ) ) ;
#82201=DIRECTION ( 'NONE',  ( 0.06975647374412546897, 0.9975640502598241977, 0.000000000000000000 ) ) ;
#82318=DIRECTION ( 'NONE',  ( -0.4771587602595986910, -0.8788171126619707119, 0.000000000000000000 ) ) ;
#82411=ADVANCED_FACE ( 'NONE', ( #69840 ), #78432, .F. ) ;
#82444=CARTESIAN_POINT ( 'NONE',  ( 0.2450472757604422180, -5.405843919193447533, 8.999999999999998224 ) ) ;
#82493=VECTOR ( 'NONE', #77965, 1000.000000000000000 ) ;
#82528=VERTEX_POINT ( 'NONE', #62235 ) ;
#82536=ORIENTED_EDGE ( 'NONE', *, *, #65712, .T. ) ;
#82548=CARTESIAN_POINT ( 'NONE',  ( -4.531374827497722357, 4.263680106169587702, 1.700000000000006839 ) ) ;
#82614=ORIENTED_EDGE ( 'NONE', *, *, #70217, .T. ) ;
#82664=DIRECTION ( 'NONE',  ( 0.06975647374412546897, 0.9975640502598241977, 0.000000000000000000 ) ) ;
#82837=ORIENTED_EDGE ( 'NONE', *, *, #6799, .T. ) ;
#82863=VERTEX_POINT ( 'NONE', #86815 ) ;
#82936=LINE ( 'NONE', #82444, #12612 ) ;
#83045=DIRECTION ( 'NONE',  ( 0.8788171126619707119, -0.4771587602595986910, 0.000000000000000000 ) ) ;
#83103=EDGE_LOOP ( 'NONE', ( #37483, #63510, #9108, #74594 ) ) ;
#83106=ORIENTED_EDGE ( 'NONE', *, *, #46709, .F. ) ;
#83325=DIRECTION ( 'NONE',  ( 0.000000000000000000, 0.000000000000000000, 1.000000000000000000 ) ) ;
#83345=ORIENTED_EDGE ( 'NONE', *, *, #64608, .T. ) ;
#83364=DIRECTION ( 'NONE',  ( 0.1478094111296165691, -0.9890158633619158257, 6.377659838150018832E-17 ) ) ;
#83675=DIRECTION ( 'NONE',  ( -4.335561085774420994E-16, -0.000000000000000000, 1.000000000000000000 ) ) ;
#83685=DIRECTION ( 'NONE',  ( 0.9762960071199348056, 0.2164396139380966033, -0.000000000000000000 ) ) ;
#83703=EDGE_LOOP ( 'NONE', ( #55980, #8415, #43225, #47438 ) ) ;
#83706=CARTESIAN_POINT ( 'NONE',  ( 0.5964549592197740946, 8.529703308962702124, -1.700000000000008837 ) ) ;
#83867=LINE ( 'NONE', #6245, #6516 ) ;
#83946=DIRECTION ( 'NONE',  ( 0.000000000000000000, -1.000000000000000000, 4.297590679709308564E-16 ) ) ;
#83955=EDGE_CURVE ( 'NONE', #1549, #1657, #48191, .T. ) ;
#84004=EDGE_LOOP ( 'NONE', ( #2154, #56032, #32863, #98259 ) ) ;
#84379=AXIS2_PLACEMENT_3D ( 'NONE', #59605, #4813, #13404 ) ;
#84521=CARTESIAN_POINT ( 'NONE',  ( -0.7395115731254252589, 18.09566585216508727, -9.000000000000000000 ) ) ;
#84683=VECTOR ( 'NONE', #87154, 999.9999999999998863 ) ;
#84766=ORIENTED_EDGE ( 'NONE', *, *, #21357, .F. ) ;
#84839=ORIENTED_EDGE ( 'NONE', *, *, #31526, .F. ) ;
#84957=CARTESIAN_POINT ( 'NONE',  ( -0.6703829557040269504, 4.102177322343282917, -2.677392948487098267E-15 ) ) ;
#85068=CARTESIAN_POINT ( 'NONE',  ( -0.7638880233336634573, -9.374108182320437521, -9.000000000000000000 ) ) ;
#85260=ORIENTED_EDGE ( 'NONE', *, *, #31526, .T. ) ;
#85276=CARTESIAN_POINT ( 'NONE',  ( 0.5999240985075874333, 1.411520799013914917, 8.999999999999987566 ) ) ;
#85483=ORIENTED_EDGE ( 'NONE', *, *, #83955, .T. ) ;
#85596=ORIENTED_EDGE ( 'NONE', *, *, #75642, .F. ) ;
#85622=EDGE_CURVE ( 'NONE', #40572, #69058, #82936, .T. ) ;
#85639=VERTEX_POINT ( 'NONE', #21529 ) ;
#85866=CYLINDRICAL_SURFACE ( 'NONE', #81686, 10.11363636363636331 ) ;
#86006=CARTESIAN_POINT ( 'NONE',  ( -1.877194073982709988, 8.794404527355018431, 9.000000000000000000 ) ) ;
#86118=ORIENTED_EDGE ( 'NONE', *, *, #67137, .F. ) ;
#86272=ORIENTED_EDGE ( 'NONE', *, *, #31566, .F. ) ;
#86345=DIRECTION ( 'NONE',  ( -1.000000000000000000, 0.000000000000000000, 0.000000000000000000 ) ) ;
#86388=VECTOR ( 'NONE', #8834, 1000.000000000000227 ) ;
#86405=ORIENTED_EDGE ( 'NONE', *, *, #64042, .F. ) ;
#86425=DIRECTION ( 'NONE',  ( -1.000000000000000000, 0.000000000000000000, -0.000000000000000000 ) ) ;
#86426=ORIENTED_EDGE ( 'NONE', *, *, #85622, .F. ) ;
#86427=ADVANCED_FACE ( 'NONE', ( #72993 ), #72491, .F. ) ;
#86481=CARTESIAN_POINT ( 'NONE',  ( -0.7395115731254252589, 18.09566585216508727, -9.000000000000000000 ) ) ;
#86484=FACE_OUTER_BOUND ( 'NONE', #76615, .T. ) ;
#86498=DIRECTION ( 'NONE',  ( 0.9975640502598241977, -0.06975647374412546897, 0.000000000000000000 ) ) ;
#86524=DIRECTION ( 'NONE',  ( 0.1478094111296165691, -0.9890158633619158257, 0.000000000000000000 ) ) ;
#86659=CARTESIAN_POINT ( 'NONE',  ( -0.3244794670026783234, -9.612687562450236811, 9.000000000000000000 ) ) ;
#86780=CARTESIAN_POINT ( 'NONE',  ( 0.01063402156994475850, -0.1430980438411110500, 9.000000000000000000 ) ) ;
#86815=CARTESIAN_POINT ( 'NONE',  ( -2.169994883066378222, 10.75358048763950869, 3.549999999999999822 ) ) ;
#87009=EDGE_LOOP ( 'NONE', ( #53991, #39638, #96267, #84839 ) ) ;
#87017=CARTESIAN_POINT ( 'NONE',  ( -0.3244794670026783234, -9.612687562450236811, 9.000000000000000000 ) ) ;
#87066=PLANE ( 'NONE',  #88992 ) ;
#87154=DIRECTION ( 'NONE',  ( 0.4771587602595988020, 0.8788171126619706008, -0.000000000000000000 ) ) ;
#87162=DIRECTION ( 'NONE',  ( 0.000000000000000000, 0.000000000000000000, -1.000000000000000000 ) ) ;
#87249=CARTESIAN_POINT ( 'NONE',  ( -0.7395115731254272573, 18.09566585216508727, 8.999999999999998224 ) ) ;
#87320=CLOSED_SHELL ( 'NONE', ( #96194, #82411, #46925, #93054, #4089, #89341, #80866, #97295, #33625, #54493, #62648, #50036, #11393, #72715, #26212, #619, #94374, #46519, #55165, #94490, #52116, #92098, #51735, #55882, #33738, #94342, #94765, #65503, #11560, #62149, #292, #74568, #6117, #100402, #64761, #63546, #56481, #86427, #76232, #64702, #47670 ) ) ;
#87349=VECTOR ( 'NONE', #46952, 1000.000000000000114 ) ;
#87467=ORIENTED_EDGE ( 'NONE', *, *, #59817, .F. ) ;
#87496=CARTESIAN_POINT ( 'NONE',  ( -1.877194073982709988, 8.794404527355018431, 9.000000000000000000 ) ) ;
#87724=ORIENTED_EDGE ( 'NONE', *, *, #45154, .F. ) ;
#87777=ORIENTED_EDGE ( 'NONE', *, *, #30994, .F. ) ;
#87844=EDGE_LOOP ( 'NONE', ( #34117, #10708, #44238, #40840 ) ) ;
#87958=EDGE_CURVE ( 'NONE', #42138, #40572, #7375, .T. ) ;
#87970=VECTOR ( 'NONE', #69584, 1000.000000000000114 ) ;
#88031=VECTOR ( 'NONE', #82664, 1000.000000000000114 ) ;
#88224=CARTESIAN_POINT ( 'NONE',  ( 0.9626393376689279524, 13.76638389358553916, 0.000000000000000000 ) ) ;
#88395=EDGE_CURVE ( 'NONE', #89454, #16487, #98603, .T. ) ;
#88469=DIRECTION ( 'NONE',  ( 0.000000000000000000, 0.000000000000000000, -1.000000000000000000 ) ) ;
#88489=PLANE ( 'NONE',  #10 ) ;
#88579=DIRECTION ( 'NONE',  ( -0.9890158633619160478, -0.1478094111296162083, 0.000000000000000000 ) ) ;
#88693=EDGE_CURVE ( 'NONE', #52065, #52789, #21849, .T. ) ;
#88868=ORIENTED_EDGE ( 'NONE', *, *, #73374, .T. ) ;
#88894=EDGE_CURVE ( 'NONE', #1657, #14465, #53397, .T. ) ;
#88992=AXIS2_PLACEMENT_3D ( 'NONE', #17557, #9438, #17051 ) ;
#89075=DIRECTION ( 'NONE',  ( 0.06975647374412546897, 0.9975640502598241977, 4.700301109882543835E-17 ) ) ;
#89118=ORIENTED_EDGE ( 'NONE', *, *, #23300, .T. ) ;
#89140=EDGE_LOOP ( 'NONE', ( #56126, #73935, #100061, #59153, #84766 ) ) ;
#89299=DIRECTION ( 'NONE',  ( -0.06975647374412549673, -0.9975640502598241977, 0.000000000000000000 ) ) ;
#89341=ADVANCED_FACE ( 'NONE', ( #29359, #76025 ), #54584, .F. ) ;
#89371=ORIENTED_EDGE ( 'NONE', *, *, #88395, .F. ) ;
#89409=EDGE_CURVE ( 'NONE', #98585, #58202, #45104, .T. ) ;
#89454=VERTEX_POINT ( 'NONE', #97139 ) ;
#89672=DIRECTION ( 'NONE',  ( 0.9975640502598243087, -0.06975647374412546897, -0.000000000000000000 ) ) ;
#89698=DIRECTION ( 'NONE',  ( 0.9762960071199348056, 0.2164396139380966033, 0.000000000000000000 ) ) ;
#89739=VERTEX_POINT ( 'NONE', #62577 ) ;
#89751=ORIENTED_EDGE ( 'NONE', *, *, #74234, .T. ) ;
#89882=LINE ( 'NONE', #10259, #10853 ) ;
#89951=( LENGTH_UNIT ( ) NAMED_UNIT ( * ) SI_UNIT ( .MILLI., .METRE. ) );
#90002=VECTOR ( 'NONE', #79997, 1000.000000000000114 ) ;
#90062=VECTOR ( 'NONE', #53921, 1000.000000000000227 ) ;
#90095=EDGE_CURVE ( 'NONE', #29853, #16487, #16272, .T. ) ;
#90220=CARTESIAN_POINT ( 'NONE',  ( -2.169994883066378222, 10.75358048763951047, -3.549999999999999822 ) ) ;
#90361=EDGE_LOOP ( 'NONE', ( #90393, #40593, #82837, #39783 ) ) ;
#90393=ORIENTED_EDGE ( 'NONE', *, *, #54883, .F. ) ;
#90695=ORIENTED_EDGE ( 'NONE', *, *, #88693, .T. ) ;
#90717=DIRECTION ( 'NONE',  ( 1.000000000000000000, 0.000000000000000000, 0.000000000000000000 ) ) ;
#90754=FACE_OUTER_BOUND ( 'NONE', #5771, .T. ) ;
#90767=CIRCLE ( 'NONE', #81065, 10.49999999999999112 ) ;
#90925=PLANE ( 'NONE',  #94741 ) ;
#91128=ORIENTED_EDGE ( 'NONE', *, *, #66468, .F. ) ;
#91144=ORIENTED_EDGE ( 'NONE', *, *, #44533, .F. ) ;
#91209=CARTESIAN_POINT ( 'NONE',  ( -2.948852648430471124, -14.44618168209107445, 0.000000000000000000 ) ) ;
#91341=EDGE_CURVE ( 'NONE', #43797, #67869, #70960, .T. ) ;
#91424=LINE ( 'NONE', #92924, #63949 ) ;
#91473=ORIENTED_EDGE ( 'NONE', *, *, #6799, .F. ) ;
#91493=ORIENTED_EDGE ( 'NONE', *, *, #40669, .T. ) ;
#91530=ORIENTED_EDGE ( 'NONE', *, *, #23680, .T. ) ;
#91737=ORIENTED_EDGE ( 'NONE', *, *, #38383, .T. ) ;
#91956=AXIS2_PLACEMENT_3D ( 'NONE', #86780, #48234, #17272 ) ;
#92098=ADVANCED_FACE ( 'NONE', ( #68635 ), #6226, .T. ) ;
#92100=EDGE_LOOP ( 'NONE', ( #26026, #44940, #90695, #2642 ) ) ;
#92126=ORIENTED_EDGE ( 'NONE', *, *, #82014, .T. ) ;
#92188=CARTESIAN_POINT ( 'NONE',  ( -1.675486951385420475, 10.82748519320431591, -3.549999999999999822 ) ) ;
#92201=EDGE_CURVE ( 'NONE', #18856, #67869, #71138, .T. ) ;
#92225=ORIENTED_EDGE ( 'NONE', *, *, #72147, .F. ) ;
#92283=EDGE_CURVE ( 'NONE', #78060, #70264, #11302, .T. ) ;
#92378=VERTEX_POINT ( 'NONE', #27956 ) ;
#92462=DIRECTION ( 'NONE',  ( -0.4771587602595987465, -0.8788171126619706008, 0.000000000000000000 ) ) ;
#92649=CARTESIAN_POINT ( 'NONE',  ( -4.209565145052936330, 8.865772972990910716, -1.700000000000008837 ) ) ;
#92740=CARTESIAN_POINT ( 'NONE',  ( 10.57556460110582286, 0.7139560615726621151, 8.999999999999984013 ) ) ;
#92771=ORIENTED_EDGE ( 'NONE', *, *, #73374, .F. ) ;
#92794=CARTESIAN_POINT ( 'NONE',  ( 10.57556460110582996, 0.7139560615726621151, -8.999999999999994671 ) ) ;
#92818=CARTESIAN_POINT ( 'NONE',  ( 3.138110291115776995, 11.54688212118755075, 3.549999999999999822 ) ) ;
#92852=ORIENTED_EDGE ( 'NONE', *, *, #62995, .T. ) ;
#92924=CARTESIAN_POINT ( 'NONE',  ( 1.255616527394258553, 17.95615290467683778, -9.000000000000000000 ) ) ;
#92964=DIRECTION ( 'NONE',  ( -0.8788171126619707119, 0.4771587602595986910, -0.000000000000000000 ) ) ;
#93054=ADVANCED_FACE ( 'NONE', ( #94604 ), #49451, .F. ) ;
#93109=ORIENTED_EDGE ( 'NONE', *, *, #12078, .T. ) ;
#93146=DIRECTION ( 'NONE',  ( 0.000000000000000000, 1.000000000000000000, 4.688851412615178005E-17 ) ) ;
#93318=DIRECTION ( 'NONE',  ( 0.000000000000000000, -1.000000000000000000, -6.307606751056558338E-17 ) ) ;
#93361=EDGE_CURVE ( 'NONE', #17858, #77501, #52432, .T. ) ;
#93449=VECTOR ( 'NONE', #44249, 1000.000000000000114 ) ;
#93489=ORIENTED_EDGE ( 'NONE', *, *, #37308, .F. ) ;
#93599=FACE_OUTER_BOUND ( 'NONE', #87844, .T. ) ;
#93741=ORIENTED_EDGE ( 'NONE', *, *, #35271, .T. ) ;
#93909=EDGE_LOOP ( 'NONE', ( #72407, #52569, #99584, #63558 ) ) ;
#94320=CYLINDRICAL_SURFACE ( 'NONE', #22448, 1.700000000000008837 ) ;
#94342=ADVANCED_FACE ( 'NONE', ( #33405 ), #94806, .T. ) ;
#94374=ADVANCED_FACE ( 'NONE', ( #13553 ), #98285, .F. ) ;
#94388=ORIENTED_EDGE ( 'NONE', *, *, #27874, .F. ) ;
#94454=FACE_OUTER_BOUND ( 'NONE', #1394, .T. ) ;
#94490=ADVANCED_FACE ( 'NONE', ( #35905 ), #52135, .F. ) ;
#94604=FACE_OUTER_BOUND ( 'NONE', #66778, .T. ) ;
#94609=VERTEX_POINT ( 'NONE', #85068 ) ;
#94741=AXIS2_PLACEMENT_3D ( 'NONE', #92794, #36638, #46139 ) ;
#94765=ADVANCED_FACE ( 'NONE', ( #69352 ), #100269, .F. ) ;
#94806=CYLINDRICAL_SURFACE ( 'NONE', #70706, 5.500000000000001776 ) ;
#94836=DIRECTION ( 'NONE',  ( 0.9975640502598241977, -0.06975647374412546897, -0.000000000000000000 ) ) ;
#94966=CARTESIAN_POINT ( 'NONE',  ( -2.814730745656462307, 14.91141199530731853, 8.673617379884035472E-16 ) ) ;
#95147=EDGE_CURVE ( 'NONE', #5623, #47484, #16425, .T. ) ;
#95175=DIRECTION ( 'NONE',  ( -0.9890158633619159367, -0.1478094111296165691, -0.000000000000000000 ) ) ;
#95323=ORIENTED_EDGE ( 'NONE', *, *, #99023, .F. ) ;
#95340=PRODUCT_DEFINITION ( 'UNKNOWN', '', #57026, #6334 ) ;
#95538=VECTOR ( 'NONE', #32564, 999.9999999999998863 ) ;
#95686=CARTESIAN_POINT ( 'NONE',  ( 1.255616527394258553, 17.95615290467683778, 9.000000000000000000 ) ) ;
#95702=ORIENTED_EDGE ( 'NONE', *, *, #6185, .T. ) ;
#95811=DIRECTION ( 'NONE',  ( 0.9975640502598243087, -0.06975647374412546897, -0.000000000000000000 ) ) ;
#96191=CARTESIAN_POINT ( 'NONE',  ( -0.7395115731254252589, 18.09566585216508727, -8.999999999999998224 ) ) ;
#96194=ADVANCED_FACE ( 'NONE', ( #19446 ), #19943, .F. ) ;
#96267=ORIENTED_EDGE ( 'NONE', *, *, #31022, .F. ) ;
#96434=LINE ( 'NONE', #58387, #60432 ) ;
#96492=DIRECTION ( 'NONE',  ( -0.9890158633619158257, -0.1478094111296165414, -0.000000000000000000 ) ) ;
#96502=CIRCLE ( 'NONE', #60881, 2.499999999999963141 ) ;
#96913=DIRECTION ( 'NONE',  ( -0.2164396139380965756, 0.9762960071199346945, 0.000000000000000000 ) ) ;
#97139=CARTESIAN_POINT ( 'NONE',  ( 0.1011420733776826480, 1.446399035885977069, -9.000000000000000000 ) ) ;
#97198=CARTESIAN_POINT ( 'NONE',  ( -1.877194073982709988, 8.794404527355018431, -9.000000000000000000 ) ) ;
#97295=ADVANCED_FACE ( 'NONE', ( #65671, #57052 ), #88489, .T. ) ;
#97414=EDGE_LOOP ( 'NONE', ( #69515, #35630, #24623, #37645 ) ) ;
#97433=CIRCLE ( 'NONE', #16364, 5.000000000000001776 ) ;
#97560=DIRECTION ( 'NONE',  ( -0.9890158633619159367, -0.1478094111296165969, 0.000000000000000000 ) ) ;
#97813=APPLICATION_CONTEXT ( 'configuration controlled 3d designs of mechanical parts and assemblies' ) ;
#97884=AXIS2_PLACEMENT_3D ( 'NONE', #20943, #58044, #74731 ) ;
#97918=CARTESIAN_POINT ( 'NONE',  ( -0.1456595461938881009, 0.5911710074084819411, -2.677392948487098267E-15 ) ) ;
#97920=VERTEX_POINT ( 'NONE', #74118 ) ;
#98029=CARTESIAN_POINT ( 'NONE',  ( -1.164890887384984586, 4.028272616778474813, 3.549999999999996714 ) ) ;
#98095=CIRCLE ( 'NONE', #5758, 1.999999999999963141 ) ;
#98129=CARTESIAN_POINT ( 'NONE',  ( -0.6703829557040269504, 4.102177322343282917, -2.677392948487098267E-15 ) ) ;
#98255=LINE ( 'NONE', #36374, #68100 ) ;
#98259=ORIENTED_EDGE ( 'NONE', *, *, #33872, .T. ) ;
#98285=PLANE ( 'NONE',  #20422 ) ;
#98292=CARTESIAN_POINT ( 'NONE',  ( -1.382686142301752019, 8.868309232919825646, 9.000000000000000000 ) ) ;
#98379=CARTESIAN_POINT ( 'NONE',  ( 0.4987820251299121543, -0.03487823687206273449, 9.000000000000000000 ) ) ;
#98416=CARTESIAN_POINT ( 'NONE',  ( -1.164890887384984586, 4.028272616778474813, -2.677392948487098267E-15 ) ) ;
#98435=AXIS2_PLACEMENT_3D ( 'NONE', #14983, #86498, #38320 ) ;
#98559=DIRECTION ( 'NONE',  ( 0.9975640502598243087, -0.06975647374412546897, -0.000000000000000000 ) ) ;
#98585=VERTEX_POINT ( 'NONE', #5361 ) ;
#98603=LINE ( 'NONE', #45336, #48555 ) ;
#98902=DIRECTION ( 'NONE',  ( 0.8788171126619707119, -0.4771587602595986910, 0.000000000000000000 ) ) ;
#99023=EDGE_CURVE ( 'NONE', #13572, #29853, #61030, .T. ) ;
#99179=ORIENTED_EDGE ( 'NONE', *, *, #72302, .T. ) ;
#99286=ORIENTED_EDGE ( 'NONE', *, *, #27112, .T. ) ;
#99506=CARTESIAN_POINT ( 'NONE',  ( 0.2450472757604422180, -5.405843919193447533, -9.000000000000000000 ) ) ;
#99553=CARTESIAN_POINT ( 'NONE',  ( -0.7395115731254252589, 18.09566585216508727, -8.999999999999998224 ) ) ;
#99583=CARTESIAN_POINT ( 'NONE',  ( 1.754398552524170762, 17.92127466780477718, 9.000000000000000000 ) ) ;
#99584=ORIENTED_EDGE ( 'NONE', *, *, #99948, .T. ) ;
#99635=ORIENTED_EDGE ( 'NONE', *, *, #18155, .F. ) ;
#99822=AXIS2_PLACEMENT_3D ( 'NONE', #51870, #17295, #567 ) ;
#99853=DIRECTION ( 'NONE',  ( 0.9762960071199348056, 0.2164396139380966033, -0.000000000000000000 ) ) ;
#99890=CYLINDRICAL_SURFACE ( 'NONE', #33425, 21.24999999999998579 ) ;
#99913=CARTESIAN_POINT ( 'NONE',  ( -1.675486951385420475, 10.82748519320431591, 0.000000000000000000 ) ) ;
#99948=EDGE_CURVE ( 'NONE', #98585, #12105, #69144, .T. ) ;
#100061=ORIENTED_EDGE ( 'NONE', *, *, #28592, .F. ) ;
#100263=CARTESIAN_POINT ( 'NONE',  ( -3.212051231530180573, 17.72614232434105119, 0.000000000000000000 ) ) ;
#100269=PLANE ( 'NONE',  #78797 ) ;
#100385=DIRECTION ( 'NONE',  ( -0.4771587602595986910, -0.8788171126619707119, 0.000000000000000000 ) ) ;
#100402=ADVANCED_FACE ( 'NONE', ( #17750 ), #71547, .F. ) ;
#100448=COLOUR_RGB('Sky Blue', 0.40784314, 0.44705882, 0.49803922);
#100449=FILL_AREA_STYLE_COLOUR('',#100448);
#100450=FILL_AREA_STYLE('',(#100449));
#100451=SURFACE_STYLE_FILL_AREA(#100450);
#100452=SURFACE_SIDE_STYLE('',(#100451));
#100453=SURFACE_STYLE_USAGE(.BOTH.,#100452);
#100454=PRESENTATION_STYLE_ASSIGNMENT((#100453));
#100496=STYLED_ITEM('',(#100454),#10173);
#100497=MECHANICAL_DESIGN_GEOMETRIC_PRESENTATION_REPRESENTATION('',(#100496),#14765);
ENDSEC;
END-ISO-10303-21;
